ISO-10303-21;
HEADER;
FILE_DESCRIPTION (('STEP AP214'),
    '1' );
FILE_NAME ('Part10^Assem2.step',
    '2026-11-01T06:29:40',
    ( '' ),
    ( '' ),
    'SwSTEP 2.0',
    'SolidWorks 2024',
    '' );
FILE_SCHEMA (( 'AUTOMOTIVE_DESIGN' ));
ENDSEC;

DATA;
#11=ORIENTED_EDGE ( 'NONE', *, *, #4617, .F. ) ;
#12=CARTESIAN_POINT ( 'NONE',  ( 153.4893729001366580, 145.9162550801369491, 0.000000000000000000 ) ) ;
#14=VECTOR ( 'NONE', #3072, 1000.000000000000000 ) ;
#17=DIRECTION ( 'NONE',  ( 0.000000000000000000, 1.000000000000000000, 0.000000000000000000 ) ) ;
#21=VERTEX_POINT ( 'NONE', #6304 ) ;
#23=CARTESIAN_POINT ( 'NONE',  ( 143.0892156028631348, 80.91625508013694912, 245.0000000000000000 ) ) ;
#25=COLOUR_RGB ( '', 0.66274510, 0.83137255, 0.94901961) ;
#27=STYLED_ITEM ( 'NONE', ( #13030 ), #7501 ) ;
#31=FACE_OUTER_BOUND ( 'NONE', #2574, .T. ) ;
#32=CARTESIAN_POINT ( 'NONE',  ( -211.5106270998635409, 123.1299228374912644, 29.36128450348865471 ) ) ;
#39=VERTEX_POINT ( 'NONE', #2353 ) ;
#44=ORIENTED_EDGE ( 'NONE', *, *, #9394, .T. ) ;
#46=ORIENTED_EDGE ( 'NONE', *, *, #5718, .T. ) ;
#49=EDGE_CURVE ( 'NONE', #6461, #198, #5065, .T. ) ;
#70=DIRECTION ( 'NONE',  ( 1.000000000000000000, 5.889072920838430686E-16, -0.000000000000000000 ) ) ;
#88=UNCERTAINTY_MEASURE_WITH_UNIT (LENGTH_MEASURE( 1.000000000000000082E-05 ), #2098, 'distance_accuracy_value', 'NONE');
#95=LINE ( 'NONE', #3199, #3080 ) ;
#105=DIRECTION ( 'NONE',  ( -1.000000000000000000, -1.595148023886719315E-16, 0.000000000000000000 ) ) ;
#109=CARTESIAN_POINT ( 'NONE',  ( -211.5106270998635409, 113.1299228374912502, 170.4174721992565082 ) ) ;
#116=FACE_OUTER_BOUND ( 'NONE', #6179, .T. ) ;
#129=CARTESIAN_POINT ( 'NONE',  ( 88.88953019741013861, 80.91625508013694912, 250.0000000000000000 ) ) ;
#149=AXIS2_PLACEMENT_3D ( 'NONE', #4026, #19876, #8780 ) ;
#150=EDGE_CURVE ( 'NONE', #4273, #9122, #5658, .T. ) ;
#152=VECTOR ( 'NONE', #13179, 1000.000000000000000 ) ;
#163=DIRECTION ( 'NONE',  ( 0.000000000000000000, -1.000000000000000000, 0.000000000000000000 ) ) ;
#164=DIRECTION ( 'NONE',  ( 1.000000000000000000, 5.889072920838430686E-16, 0.000000000000000000 ) ) ;
#171=ORIENTED_EDGE ( 'NONE', *, *, #8727, .T. ) ;
#182=CYLINDRICAL_SURFACE ( 'NONE', #18527, 10.00000000000000888 ) ;
#191=DIRECTION ( 'NONE',  ( 1.000000000000000000, 0.000000000000000000, 0.000000000000000000 ) ) ;
#192=ADVANCED_FACE ( 'NONE', ( #16149 ), #14568, .F. ) ;
#198=VERTEX_POINT ( 'NONE', #11872 ) ;
#200=ORIENTED_EDGE ( 'NONE', *, *, #10989, .T. ) ;
#201=ORIENTED_EDGE ( 'NONE', *, *, #1906, .T. ) ;
#206=LINE ( 'NONE', #303, #6567 ) ;
#217=CARTESIAN_POINT ( 'NONE',  ( 78.48937290013660117, 103.1299228374914065, 79.58252780074349175 ) ) ;
#221=EDGE_LOOP ( 'NONE', ( #13172, #3840 ) ) ;
#234=CARTESIAN_POINT ( 'NONE',  ( -211.5106270998635409, 113.1299228374912502, 79.58252780074349175 ) ) ;
#243=VERTEX_POINT ( 'NONE', #16917 ) ;
#244=ORIENTED_EDGE ( 'NONE', *, *, #4195, .F. ) ;
#250=CARTESIAN_POINT ( 'NONE',  ( 178.4893729001365443, 145.9162550801369491, 0.000000000000000000 ) ) ;
#254=SURFACE_STYLE_USAGE ( .BOTH. , #15843 ) ;
#255=CARTESIAN_POINT ( 'NONE',  ( 178.4893729001365728, 113.1299228374914918, 79.58252780074349175 ) ) ;
#256=( NAMED_UNIT ( * ) SI_UNIT ( $, .STERADIAN. ) SOLID_ANGLE_UNIT ( ) );
#270=VERTEX_POINT ( 'NONE', #20189 ) ;
#280=AXIS2_PLACEMENT_3D ( 'NONE', #12196, #10356, #7366 ) ;
#285=CARTESIAN_POINT ( 'NONE',  ( 78.48937290013660117, 113.1299228374914208, 170.4174721992565082 ) ) ;
#303=CARTESIAN_POINT ( 'NONE',  ( 153.4893729001366580, 0.000000000000000000, 250.0000000000000000 ) ) ;
#309=MECHANICAL_DESIGN_GEOMETRIC_PRESENTATION_REPRESENTATION('',(#4258),#18737);
#312=DIRECTION ( 'NONE',  ( -1.000000000000000000, 0.000000000000000000, 0.000000000000000000 ) ) ;
#313=CARTESIAN_POINT ( 'NONE',  ( 178.4893729001365728, 123.1299228374914918, 170.4174721992565082 ) ) ;
#314=EDGE_CURVE ( 'NONE', #4687, #4967, #10617, .T. ) ;
#320=DIRECTION ( 'NONE',  ( 1.000000000000000000, 5.889072920838430686E-16, -0.000000000000000000 ) ) ;
#328=SURFACE_STYLE_FILL_AREA ( #17952 ) ;
#335=FILL_AREA_STYLE ('',( #16240 ) ) ;
#336=MECHANICAL_DESIGN_GEOMETRIC_PRESENTATION_REPRESENTATION('',(#16173),#16815);
#339=( GEOMETRIC_REPRESENTATION_CONTEXT ( 3 ) GLOBAL_UNCERTAINTY_ASSIGNED_CONTEXT ( ( #10174 ) ) GLOBAL_UNIT_ASSIGNED_CONTEXT ( ( #15376, #15481, #12696 ) ) REPRESENTATION_CONTEXT ( 'NONE', 'WORKASPACE' ) );
#343=ADVANCED_FACE ( 'NONE', ( #12380 ), #5984, .F. ) ;
#345=VERTEX_POINT ( 'NONE', #3296 ) ;
#348=DIRECTION ( 'NONE',  ( 1.000000000000000000, 5.889072920838430686E-16, -0.000000000000000000 ) ) ;
#351=EDGE_LOOP ( 'NONE', ( #10484, #6293, #12449, #14964, #16000, #5547 ) ) ;
#364=ORIENTED_EDGE ( 'NONE', *, *, #8997, .T. ) ;
#370=EDGE_CURVE ( 'NONE', #3638, #20118, #95, .T. ) ;
#378=DIRECTION ( 'NONE',  ( 1.000000000000000000, 9.815121534730717399E-17, -0.000000000000000000 ) ) ;
#379=PLANE ( 'NONE',  #17601 ) ;
#383=PRESENTATION_STYLE_ASSIGNMENT (( #8528 ) ) ;
#386=ORIENTED_EDGE ( 'NONE', *, *, #7319, .F. ) ;
#398=FACE_BOUND ( 'NONE', #13239, .T. ) ;
#400=CIRCLE ( 'NONE', #7646, 10.00000000000000888 ) ;
#402=AXIS2_PLACEMENT_3D ( 'NONE', #2225, #6812, #5247 ) ;
#419=CIRCLE ( 'NONE', #2387, 10.00000000000000888 ) ;
#428=FACE_BOUND ( 'NONE', #9334, .T. ) ;
#437=( NAMED_UNIT ( * ) PLANE_ANGLE_UNIT ( ) SI_UNIT ( $, .RADIAN. ) );
#443=EDGE_CURVE ( 'NONE', #39, #16841, #11331, .T. ) ;
#445=EDGE_LOOP ( 'NONE', ( #12077, #5510, #14819, #478 ) ) ;
#447=EDGE_LOOP ( 'NONE', ( #14456, #1274 ) ) ;
#449=UNCERTAINTY_MEASURE_WITH_UNIT (LENGTH_MEASURE( 1.000000000000000082E-05 ), #13048, 'distance_accuracy_value', 'NONE');
#461=FACE_BOUND ( 'NONE', #14046, .T. ) ;
#463=( NAMED_UNIT ( * ) PLANE_ANGLE_UNIT ( ) SI_UNIT ( $, .RADIAN. ) );
#472=AXIS2_PLACEMENT_3D ( 'NONE', #19365, #14841, #16413 ) ;
#478=ORIENTED_EDGE ( 'NONE', *, *, #4617, .T. ) ;
#513=VECTOR ( 'NONE', #10974, 1000.000000000000000 ) ;
#525=VECTOR ( 'NONE', #6100, 1000.000000000000000 ) ;
#530=VERTEX_POINT ( 'NONE', #5261 ) ;
#531=DIRECTION ( 'NONE',  ( -0.000000000000000000, -1.000000000000000000, -0.000000000000000000 ) ) ;
#533=ORIENTED_EDGE ( 'NONE', *, *, #18599, .F. ) ;
#540=PRESENTATION_STYLE_ASSIGNMENT (( #9923 ) ) ;
#541=CYLINDRICAL_SURFACE ( 'NONE', #732, 10.00000000000000888 ) ;
#542=DIRECTION ( 'NONE',  ( 0.000000000000000000, 0.000000000000000000, -1.000000000000000000 ) ) ;
#545=CYLINDRICAL_SURFACE ( 'NONE', #13470, 10.00000000000000888 ) ;
#547=PLANE ( 'NONE',  #5073 ) ;
#553=ADVANCED_FACE ( 'NONE', ( #16403 ), #14824, .F. ) ;
#555=FILL_AREA_STYLE ('',( #14994 ) ) ;
#557=ORIENTED_EDGE ( 'NONE', *, *, #314, .F. ) ;
#562=DIRECTION ( 'NONE',  ( 0.000000000000000000, 1.000000000000000000, 0.000000000000000000 ) ) ;
#569=DIRECTION ( 'NONE',  ( 1.000000000000000000, 9.815121534730717399E-17, -0.000000000000000000 ) ) ;
#582=LINE ( 'NONE', #6893, #152 ) ;
#590=CARTESIAN_POINT ( 'NONE',  ( 178.4893729001365728, 123.1299228374914918, 220.6387154965113382 ) ) ;
#598=EDGE_CURVE ( 'NONE', #5524, #14262, #8850, .T. ) ;
#600=EDGE_LOOP ( 'NONE', ( #18640, #5811 ) ) ;
#601=CARTESIAN_POINT ( 'NONE',  ( 78.48937290013660117, 113.1299228374914208, 79.58252780074349175 ) ) ;
#615=CARTESIAN_POINT ( 'NONE',  ( 153.4893729001366864, 123.1299228374914634, 29.36128450348865471 ) ) ;
#618=ORIENTED_EDGE ( 'NONE', *, *, #12060, .T. ) ;
#629=CARTESIAN_POINT ( 'NONE',  ( 153.4893729001366580, 80.91625508013694912, 250.0000000000000000 ) ) ;
#636=DIRECTION ( 'NONE',  ( 0.000000000000000000, 1.000000000000000000, 0.000000000000000000 ) ) ;
#654=FILL_AREA_STYLE ('',( #11708 ) ) ;
#663=PLANE ( 'NONE',  #3342 ) ;
#669=EDGE_LOOP ( 'NONE', ( #5288, #16345, #8845, #9918 ) ) ;
#674=ORIENTED_EDGE ( 'NONE', *, *, #1549, .F. ) ;
#686=UNCERTAINTY_MEASURE_WITH_UNIT (LENGTH_MEASURE( 1.000000000000000082E-05 ), #915, 'distance_accuracy_value', 'NONE');
#697=DIRECTION ( 'NONE',  ( -1.000000000000000000, 0.000000000000000000, -0.000000000000000000 ) ) ;
#707=CARTESIAN_POINT ( 'NONE',  ( 143.0892156028631348, 80.91625508013694912, 245.0000000000000000 ) ) ;
#708=AXIS2_PLACEMENT_3D ( 'NONE', #14152, #7971, #18986 ) ;
#722=CARTESIAN_POINT ( 'NONE',  ( 98.48937290013662960, 1.571051285554951424E-14, -97.94896630388704750 ) ) ;
#724=CARTESIAN_POINT ( 'NONE',  ( 153.4893729001366864, 113.1299228374914634, 79.58252780074349175 ) ) ;
#726=( NAMED_UNIT ( * ) PLANE_ANGLE_UNIT ( ) SI_UNIT ( $, .RADIAN. ) );
#732=AXIS2_PLACEMENT_3D ( 'NONE', #13342, #19587, #11368 ) ;
#736=ADVANCED_FACE ( 'NONE', ( #6582 ), #17594, .F. ) ;
#738=VERTEX_POINT ( 'NONE', #11105 ) ;
#747=( GEOMETRIC_REPRESENTATION_CONTEXT ( 3 ) GLOBAL_UNCERTAINTY_ASSIGNED_CONTEXT ( ( #13224 ) ) GLOBAL_UNIT_ASSIGNED_CONTEXT ( ( #19279, #14431, #19158 ) ) REPRESENTATION_CONTEXT ( 'NONE', 'WORKASPACE' ) );
#756=FILL_AREA_STYLE_COLOUR ( '', #7055 ) ;
#759=VECTOR ( 'NONE', #16819, 1000.000000000000000 ) ;
#779=DIRECTION ( 'NONE',  ( -1.000000000000000000, -0.000000000000000000, -0.000000000000000000 ) ) ;
#780=LINE ( 'NONE', #3692, #4544 ) ;
#783=VECTOR ( 'NONE', #8885, 1000.000000000000000 ) ;
#785=VECTOR ( 'NONE', #5066, 1000.000000000000000 ) ;
#788=SURFACE_STYLE_FILL_AREA ( #11933 ) ;
#791=EDGE_CURVE ( 'NONE', #8200, #19572, #14315, .T. ) ;
#794=VECTOR ( 'NONE', #14802, 1000.000000000000000 ) ;
#800=MECHANICAL_DESIGN_GEOMETRIC_PRESENTATION_REPRESENTATION('',(#14301),#15294);
#805=EDGE_CURVE ( 'NONE', #8633, #7485, #11007, .T. ) ;
#813=LINE ( 'NONE', #2155, #3205 ) ;
#814=DIRECTION ( 'NONE',  ( 1.000000000000000000, 5.889072920838430686E-16, -0.000000000000000000 ) ) ;
#819=EDGE_CURVE ( 'NONE', #16767, #4371, #5034, .T. ) ;
#823=STYLED_ITEM ( 'NONE', ( #3664 ), #14509 ) ;
#825=VERTEX_POINT ( 'NONE', #15764 ) ;
#836=CARTESIAN_POINT ( 'NONE',  ( 53.48937290013658696, 113.1299228374914065, 79.58252780074349175 ) ) ;
#847=EDGE_CURVE ( 'NONE', #1341, #4687, #19625, .T. ) ;
#852=ORIENTED_EDGE ( 'NONE', *, *, #8790, .F. ) ;
#853=PLANE ( 'NONE',  #17110 ) ;
#858=LINE ( 'NONE', #8307, #16439 ) ;
#862=FILL_AREA_STYLE_COLOUR ( '', #8842 ) ;
#864=( LENGTH_UNIT ( ) NAMED_UNIT ( * ) SI_UNIT ( .MILLI., .METRE. ) );
#883=PLANE ( 'NONE',  #10834 ) ;
#898=AXIS2_PLACEMENT_3D ( 'NONE', #20061, #4230, #15564 ) ;
#900=DIRECTION ( 'NONE',  ( -1.000000000000000000, 0.000000000000000000, 0.000000000000000000 ) ) ;
#912=FILL_AREA_STYLE_COLOUR ( '', #15271 ) ;
#915=( LENGTH_UNIT ( ) NAMED_UNIT ( * ) SI_UNIT ( .MILLI., .METRE. ) );
#923=EDGE_CURVE ( 'NONE', #1858, #17019, #582, .T. ) ;
#926=DIRECTION ( 'NONE',  ( 0.000000000000000000, 1.000000000000000000, -0.000000000000000000 ) ) ;
#938=SURFACE_SIDE_STYLE ('',( #10546 ) ) ;
#945=( NAMED_UNIT ( * ) SI_UNIT ( $, .STERADIAN. ) SOLID_ANGLE_UNIT ( ) );
#946=LINE ( 'NONE', #5713, #10536 ) ;
#947=( NAMED_UNIT ( * ) SI_UNIT ( $, .STERADIAN. ) SOLID_ANGLE_UNIT ( ) );
#956=EDGE_LOOP ( 'NONE', ( #11937, #5518, #5980, #6334 ) ) ;
#990=FILL_AREA_STYLE ('',( #15565 ) ) ;
#991=FILL_AREA_STYLE_COLOUR ( '', #3961 ) ;
#993=DIRECTION ( 'NONE',  ( -1.000000000000000000, -2.135044278125301096E-16, -0.000000000000000000 ) ) ;
#995=VERTEX_POINT ( 'NONE', #13761 ) ;
#1001=UNCERTAINTY_MEASURE_WITH_UNIT (LENGTH_MEASURE( 1.000000000000000082E-05 ), #13552, 'distance_accuracy_value', 'NONE');
#1002=EDGE_CURVE ( 'NONE', #10163, #19309, #15997, .T. ) ;
#1005=DIRECTION ( 'NONE',  ( -0.000000000000000000, 0.000000000000000000, 1.000000000000000000 ) ) ;
#1013=CYLINDRICAL_SURFACE ( 'NONE', #11952, 10.00000000000000888 ) ;
#1023=UNCERTAINTY_MEASURE_WITH_UNIT (LENGTH_MEASURE( 1.000000000000000082E-05 ), #15714, 'distance_accuracy_value', 'NONE');
#1026=DIRECTION ( 'NONE',  ( -0.000000000000000000, 0.000000000000000000, 1.000000000000000000 ) ) ;
#1031=DIRECTION ( 'NONE',  ( -0.000000000000000000, 0.000000000000000000, 1.000000000000000000 ) ) ;
#1034=EDGE_CURVE ( 'NONE', #17019, #15858, #12629, .T. ) ;
#1037=( NAMED_UNIT ( * ) SI_UNIT ( $, .STERADIAN. ) SOLID_ANGLE_UNIT ( ) );
#1038=DIRECTION ( 'NONE',  ( 1.000000000000000000, -0.000000000000000000, 0.000000000000000000 ) ) ;
#1040=CARTESIAN_POINT ( 'NONE',  ( 0.000000000000000000, 167.9162550801369491, -97.94896630388704750 ) ) ;
#1053=DIRECTION ( 'NONE',  ( 0.000000000000000000, 0.000000000000000000, -1.000000000000000000 ) ) ;
#1058=VERTEX_POINT ( 'NONE', #3350 ) ;
#1062=CARTESIAN_POINT ( 'NONE',  ( 0.000000000000000000, 145.9162550801369491, 0.000000000000000000 ) ) ;
#1069=SURFACE_SIDE_STYLE ('',( #16782 ) ) ;
#1076=EDGE_CURVE ( 'NONE', #11219, #16393, #1461, .T. ) ;
#1080=AXIS2_PLACEMENT_3D ( 'NONE', #15697, #15784, #1522 ) ;
#1086=FACE_OUTER_BOUND ( 'NONE', #15879, .T. ) ;
#1092=LINE ( 'NONE', #7612, #18888 ) ;
#1093=STYLED_ITEM ( 'NONE', ( #4255 ), #15737 ) ;
#1094=CARTESIAN_POINT ( 'NONE',  ( -211.5106270998635409, 103.1299228374912360, 79.58252780074349175 ) ) ;
#1097=( GEOMETRIC_REPRESENTATION_CONTEXT ( 3 ) GLOBAL_UNCERTAINTY_ASSIGNED_CONTEXT ( ( #2702 ) ) GLOBAL_UNIT_ASSIGNED_CONTEXT ( ( #7069, #15808, #7770 ) ) REPRESENTATION_CONTEXT ( 'NONE', 'WORKASPACE' ) );
#1110=ORIENTED_EDGE ( 'NONE', *, *, #4493, .F. ) ;
#1114=CARTESIAN_POINT ( 'NONE',  ( -211.5106270998635409, 113.1299228374912502, 79.58252780074349175 ) ) ;
#1116=CARTESIAN_POINT ( 'NONE',  ( -211.5106270998635409, 123.1299228374912644, 220.6387154965113382 ) ) ;
#1136=CARTESIAN_POINT ( 'NONE',  ( 149.0892156028631348, 167.9162550801369491, 245.0000000000000000 ) ) ;
#1146=ORIENTED_EDGE ( 'NONE', *, *, #16628, .T. ) ;
#1147=FILL_AREA_STYLE ('',( #15312 ) ) ;
#1159=CIRCLE ( 'NONE', #12731, 10.00000000000000888 ) ;
#1174=DIRECTION ( 'NONE',  ( 0.000000000000000000, 0.000000000000000000, 1.000000000000000000 ) ) ;
#1175=EDGE_CURVE ( 'NONE', #4977, #1058, #16445, .T. ) ;
#1183=EDGE_LOOP ( 'NONE', ( #3020, #10540 ) ) ;
#1200=ORIENTED_EDGE ( 'NONE', *, *, #12080, .T. ) ;
#1204=STYLED_ITEM ( 'NONE', ( #4420 ), #12124 ) ;
#1224=FACE_BOUND ( 'NONE', #11623, .T. ) ;
#1228=SURFACE_STYLE_FILL_AREA ( #10749 ) ;
#1233=ORIENTED_EDGE ( 'NONE', *, *, #4236, .F. ) ;
#1234=CYLINDRICAL_SURFACE ( 'NONE', #19677, 10.00000000000000888 ) ;
#1235=( LENGTH_UNIT ( ) NAMED_UNIT ( * ) SI_UNIT ( .MILLI., .METRE. ) );
#1238=ORIENTED_EDGE ( 'NONE', *, *, #15682, .T. ) ;
#1245=ORIENTED_EDGE ( 'NONE', *, *, #20310, .T. ) ;
#1247=VERTEX_POINT ( 'NONE', #8586 ) ;
#1271=VECTOR ( 'NONE', #18931, 1000.000000000000000 ) ;
#1273=COLOUR_RGB ( '', 0.66274510, 0.83137255, 0.94901961) ;
#1274=ORIENTED_EDGE ( 'NONE', *, *, #14830, .T. ) ;
#1288=CARTESIAN_POINT ( 'NONE',  ( 53.48937290013659407, 145.9162550801369491, 250.0000000000000000 ) ) ;
#1293=EDGE_CURVE ( 'NONE', #10363, #243, #10644, .T. ) ;
#1296=ORIENTED_EDGE ( 'NONE', *, *, #11649, .T. ) ;
#1300=ORIENTED_EDGE ( 'NONE', *, *, #8914, .T. ) ;
#1307=PRODUCT_DEFINITION_SHAPE ( 'NONE', 'NONE',  #15412 ) ;
#1309=DIRECTION ( 'NONE',  ( 1.595148023886719315E-16, -1.000000000000000000, 0.000000000000000000 ) ) ;
#1314=CARTESIAN_POINT ( 'NONE',  ( 98.48937290013662960, 113.1299228374914350, 79.58252780074349175 ) ) ;
#1315=SURFACE_STYLE_USAGE ( .BOTH. , #11987 ) ;
#1321=ADVANCED_FACE ( 'NONE', ( #15089 ), #18364, .F. ) ;
#1329=MANIFOLD_SOLID_BREP ( 'Cut-Extrude4[1]', #11290 ) ;
#1334=ORIENTED_EDGE ( 'NONE', *, *, #3903, .F. ) ;
#1341=VERTEX_POINT ( 'NONE', #20318 ) ;
#1362=DIRECTION ( 'NONE',  ( -1.000000000000000000, 0.000000000000000000, 0.000000000000000000 ) ) ;
#1368=MANIFOLD_SOLID_BREP ( 'Cut-Extrude3[3]', #4719 ) ;
#1369=( LENGTH_UNIT ( ) NAMED_UNIT ( * ) SI_UNIT ( .MILLI., .METRE. ) );
#1373=LINE ( 'NONE', #17379, #11528 ) ;
#1378=AXIS2_PLACEMENT_3D ( 'NONE', #9230, #6052, #7499 ) ;
#1383=FILL_AREA_STYLE_COLOUR ( '', #3179 ) ;
#1396=MECHANICAL_DESIGN_GEOMETRIC_PRESENTATION_REPRESENTATION('',(#8668),#10314);
#1398=DIRECTION ( 'NONE',  ( -0.000000000000000000, -0.000000000000000000, 1.000000000000000000 ) ) ;
#1413=ORIENTED_EDGE ( 'NONE', *, *, #15982, .T. ) ;
#1418=EDGE_CURVE ( 'NONE', #11661, #14090, #14138, .T. ) ;
#1428=( GEOMETRIC_REPRESENTATION_CONTEXT ( 3 ) GLOBAL_UNCERTAINTY_ASSIGNED_CONTEXT ( ( #10240 ) ) GLOBAL_UNIT_ASSIGNED_CONTEXT ( ( #8408, #3862, #11796 ) ) REPRESENTATION_CONTEXT ( 'NONE', 'WORKASPACE' ) );
#1437=VECTOR ( 'NONE', #17221, 1000.000000000000000 ) ;
#1447=SURFACE_SIDE_STYLE ('',( #15609 ) ) ;
#1454=DIRECTION ( 'NONE',  ( 1.000000000000000000, 5.889072920838430686E-16, -0.000000000000000000 ) ) ;
#1461=CIRCLE ( 'NONE', #11979, 10.00000000000000888 ) ;
#1466=ORIENTED_EDGE ( 'NONE', *, *, #9563, .F. ) ;
#1470=ORIENTED_EDGE ( 'NONE', *, *, #49, .F. ) ;
#1486=SHAPE_REPRESENTATION_RELATIONSHIP ( 'NONE' , 'NONE' ,  #3934, #2502 ) ;
#1496=ORIENTED_EDGE ( 'NONE', *, *, #20213, .F. ) ;
#1508=DIRECTION ( 'NONE',  ( 0.000000000000000000, 0.000000000000000000, 1.000000000000000000 ) ) ;
#1514=EDGE_LOOP ( 'NONE', ( #16962, #17333, #16515, #11968 ) ) ;
#1516=MANIFOLD_SOLID_BREP ( 'Cut-Extrude4[2]', #9986 ) ;
#1520=EDGE_LOOP ( 'NONE', ( #17313, #11194, #200, #9789 ) ) ;
#1522=DIRECTION ( 'NONE',  ( 0.000000000000000000, 1.000000000000000000, 0.000000000000000000 ) ) ;
#1540=EDGE_CURVE ( 'NONE', #10177, #15780, #7335, .T. ) ;
#1549=EDGE_CURVE ( 'NONE', #20243, #4620, #19584, .T. ) ;
#1554=VECTOR ( 'NONE', #19834, 1000.000000000000000 ) ;
#1567=MECHANICAL_DESIGN_GEOMETRIC_PRESENTATION_REPRESENTATION('',(#7848),#4239);
#1570=ORIENTED_EDGE ( 'NONE', *, *, #10636, .T. ) ;
#1574=CARTESIAN_POINT ( 'NONE',  ( 88.88953019741013861, 167.9162550801369491, 250.0000000000000000 ) ) ;
#1600=SURFACE_SIDE_STYLE ('',( #1708 ) ) ;
#1601=EDGE_CURVE ( 'NONE', #19572, #13442, #16636, .T. ) ;
#1612=ORIENTED_EDGE ( 'NONE', *, *, #4108, .T. ) ;
#1627=EDGE_CURVE ( 'NONE', #4612, #995, #10672, .T. ) ;
#1665=VERTEX_POINT ( 'NONE', #6197 ) ;
#1668=EDGE_CURVE ( 'NONE', #12058, #16534, #7930, .T. ) ;
#1669=ORIENTED_EDGE ( 'NONE', *, *, #10572, .T. ) ;
#1679=FACE_OUTER_BOUND ( 'NONE', #12164, .T. ) ;
#1681=VERTEX_POINT ( 'NONE', #14020 ) ;
#1684=DIRECTION ( 'NONE',  ( 1.000000000000000000, 9.815121534730717399E-17, -0.000000000000000000 ) ) ;
#1695=ORIENTED_EDGE ( 'NONE', *, *, #8362, .F. ) ;
#1708=SURFACE_STYLE_FILL_AREA ( #15769 ) ;
#1719=FACE_OUTER_BOUND ( 'NONE', #956, .T. ) ;
#1731=DIRECTION ( 'NONE',  ( 0.000000000000000000, 0.000000000000000000, 1.000000000000000000 ) ) ;
#1746=SURFACE_SIDE_STYLE ('',( #18665 ) ) ;
#1750=ORIENTED_EDGE ( 'NONE', *, *, #9563, .T. ) ;
#1751=VECTOR ( 'NONE', #12600, 1000.000000000000000 ) ;
#1756=DIRECTION ( 'NONE',  ( 0.000000000000000000, 0.000000000000000000, 1.000000000000000000 ) ) ;
#1765=VECTOR ( 'NONE', #13348, 1000.000000000000000 ) ;
#1772=VECTOR ( 'NONE', #10430, 1000.000000000000000 ) ;
#1786=ORIENTED_EDGE ( 'NONE', *, *, #9186, .F. ) ;
#1787=CARTESIAN_POINT ( 'NONE',  ( -0.000000000000000000, 80.91625508013694912, 0.000000000000000000 ) ) ;
#1823=ORIENTED_EDGE ( 'NONE', *, *, #14062, .T. ) ;
#1825=SURFACE_STYLE_USAGE ( .BOTH. , #1600 ) ;
#1828=DIRECTION ( 'NONE',  ( 1.000000000000000000, 5.889072920838430686E-16, -0.000000000000000000 ) ) ;
#1838=AXIS2_PLACEMENT_3D ( 'NONE', #13789, #20276, #12067 ) ;
#1858=VERTEX_POINT ( 'NONE', #14540 ) ;
#1869=VERTEX_POINT ( 'NONE', #615 ) ;
#1890=FILL_AREA_STYLE_COLOUR ( '', #6584 ) ;
#1906=EDGE_CURVE ( 'NONE', #7140, #19410, #13350, .T. ) ;
#1918=SURFACE_STYLE_FILL_AREA ( #6815 ) ;
#1937=SURFACE_STYLE_USAGE ( .BOTH. , #11647 ) ;
#1953=EDGE_LOOP ( 'NONE', ( #18743, #4944 ) ) ;
#1967=SURFACE_SIDE_STYLE ('',( #9931 ) ) ;
#1970=COLOUR_RGB ( '', 0.72549020, 0.75294118, 0.79215686) ;
#1985=CARTESIAN_POINT ( 'NONE',  ( 78.48937290013661539, 80.91625508013694912, 250.0000000000000000 ) ) ;
#1991=ORIENTED_EDGE ( 'NONE', *, *, #6654, .T. ) ;
#2011=DIRECTION ( 'NONE',  ( 1.000000000000000000, 0.000000000000000000, 0.000000000000000000 ) ) ;
#2017=CARTESIAN_POINT ( 'NONE',  ( 78.48937290013660117, 123.1299228374914208, 170.4174721992565082 ) ) ;
#2020=CARTESIAN_POINT ( 'NONE',  ( -211.5106270998635409, 103.1299228374912360, 170.4174721992565082 ) ) ;
#2045=EDGE_CURVE ( 'NONE', #3236, #7608, #4215, .T. ) ;
#2049=UNCERTAINTY_MEASURE_WITH_UNIT (LENGTH_MEASURE( 1.000000000000000082E-05 ), #5162, 'distance_accuracy_value', 'NONE');
#2059=FACE_OUTER_BOUND ( 'NONE', #11379, .T. ) ;
#2071=CARTESIAN_POINT ( 'NONE',  ( 133.4893729001365443, 113.1299228374914634, 170.4174721992565082 ) ) ;
#2073=CIRCLE ( 'NONE', #17225, 10.00000000000000888 ) ;
#2075=SURFACE_STYLE_USAGE ( .BOTH. , #1967 ) ;
#2079=ORIENTED_EDGE ( 'NONE', *, *, #16300, .T. ) ;
#2089=PLANE ( 'NONE',  #17912 ) ;
#2098=( LENGTH_UNIT ( ) NAMED_UNIT ( * ) SI_UNIT ( .MILLI., .METRE. ) );
#2103=CARTESIAN_POINT ( 'NONE',  ( 53.48937290013658696, 113.1299228374914065, 170.4174721992565082 ) ) ;
#2112=VECTOR ( 'NONE', #8465, 1000.000000000000000 ) ;
#2114=AXIS2_PLACEMENT_3D ( 'NONE', #6728, #10200, #18025 ) ;
#2115=VERTEX_POINT ( 'NONE', #1136 ) ;
#2128=CARTESIAN_POINT ( 'NONE',  ( 133.4893729001365443, 103.1299228374914492, 79.58252780074349175 ) ) ;
#2133=FACE_OUTER_BOUND ( 'NONE', #18239, .T. ) ;
#2136=( NAMED_UNIT ( * ) SI_UNIT ( $, .STERADIAN. ) SOLID_ANGLE_UNIT ( ) );
#2139=PRESENTATION_STYLE_ASSIGNMENT (( #19140 ) ) ;
#2147=ORIENTED_EDGE ( 'NONE', *, *, #11417, .F. ) ;
#2155=CARTESIAN_POINT ( 'NONE',  ( 178.4893729001365443, 145.9162550801369491, 250.0000000000000000 ) ) ;
#2167=CARTESIAN_POINT ( 'NONE',  ( 153.4893729001366864, 113.1299228374914634, 79.58252780074349175 ) ) ;
#2169=CARTESIAN_POINT ( 'NONE',  ( 88.88953019741013861, 167.9162550801369491, 245.0000000000000000 ) ) ;
#2171=( NAMED_UNIT ( * ) PLANE_ANGLE_UNIT ( ) SI_UNIT ( $, .RADIAN. ) );
#2172=PRESENTATION_STYLE_ASSIGNMENT (( #11364 ) ) ;
#2179=DIRECTION ( 'NONE',  ( 1.000000000000000000, 5.889072920838430686E-16, -0.000000000000000000 ) ) ;
#2184=EDGE_CURVE ( 'NONE', #9454, #10177, #4360, .T. ) ;
#2188=LINE ( 'NONE', #7328, #7773 ) ;
#2191=FILL_AREA_STYLE ('',( #8491 ) ) ;
#2197=DIRECTION ( 'NONE',  ( 1.000000000000000000, 5.889072920838430686E-16, -0.000000000000000000 ) ) ;
#2202=( LENGTH_UNIT ( ) NAMED_UNIT ( * ) SI_UNIT ( .MILLI., .METRE. ) );
#2204=CARTESIAN_POINT ( 'NONE',  ( 0.000000000000000000, 0.000000000000000000, 250.0000000000000000 ) ) ;
#2210=CIRCLE ( 'NONE', #4540, 10.00000000000000888 ) ;
#2213=ORIENTED_EDGE ( 'NONE', *, *, #11649, .F. ) ;
#2215=CARTESIAN_POINT ( 'NONE',  ( 78.48937290013660117, 113.1299228374914208, 29.36128450348865471 ) ) ;
#2217=EDGE_CURVE ( 'NONE', #17253, #19266, #15504, .T. ) ;
#2225=CARTESIAN_POINT ( 'NONE',  ( -211.5106270998635409, 113.1299228374912502, 170.4174721992565082 ) ) ;
#2242=FACE_BOUND ( 'NONE', #4408, .T. ) ;
#2249=CIRCLE ( 'NONE', #5256, 10.00000000000000888 ) ;
#2251=ORIENTED_EDGE ( 'NONE', *, *, #15471, .T. ) ;
#2253=UNCERTAINTY_MEASURE_WITH_UNIT (LENGTH_MEASURE( 1.000000000000000082E-05 ), #1235, 'distance_accuracy_value', 'NONE');
#2256=ORIENTED_EDGE ( 'NONE', *, *, #923, .T. ) ;
#2259=MECHANICAL_DESIGN_GEOMETRIC_PRESENTATION_REPRESENTATION('',(#20025),#2930);
#2272=PRESENTATION_STYLE_ASSIGNMENT (( #2075 ) ) ;
#2284=CARTESIAN_POINT ( 'NONE',  ( 178.4893729001365443, 145.9162550801369491, -97.94896630388704750 ) ) ;
#2290=DIRECTION ( 'NONE',  ( 0.000000000000000000, 1.000000000000000000, 0.000000000000000000 ) ) ;
#2296=STYLED_ITEM ( 'NONE', ( #7043 ), #6214 ) ;
#2302=CARTESIAN_POINT ( 'NONE',  ( 53.48937290013658696, 113.1299228374914065, 220.6387154965113382 ) ) ;
#2303=FACE_OUTER_BOUND ( 'NONE', #14795, .T. ) ;
#2306=ORIENTED_EDGE ( 'NONE', *, *, #17461, .F. ) ;
#2307=CARTESIAN_POINT ( 'NONE',  ( 0.000000000000000000, 0.000000000000000000, 245.0000000000000000 ) ) ;
#2347=ADVANCED_FACE ( 'NONE', ( #9819, #11062, #16128, #428, #6746 ), #19294, .F. ) ;
#2353=CARTESIAN_POINT ( 'NONE',  ( 178.4893729001365443, 145.9162550801369491, 250.0000000000000000 ) ) ;
#2354=LINE ( 'NONE', #17068, #14251 ) ;
#2356=CYLINDRICAL_SURFACE ( 'NONE', #6033, 10.00000000000000888 ) ;
#2360=AXIS2_PLACEMENT_3D ( 'NONE', #18287, #16669, #20013 ) ;
#2373=( NAMED_UNIT ( * ) SI_UNIT ( $, .STERADIAN. ) SOLID_ANGLE_UNIT ( ) );
#2378=CARTESIAN_POINT ( 'NONE',  ( 53.48937290013659407, 167.9162550801369491, -97.94896630388704750 ) ) ;
#2382=ORIENTED_EDGE ( 'NONE', *, *, #10228, .T. ) ;
#2383=DIRECTION ( 'NONE',  ( 1.000000000000000000, -0.000000000000000000, 0.000000000000000000 ) ) ;
#2387=AXIS2_PLACEMENT_3D ( 'NONE', #15853, #17278, #17377 ) ;
#2394=FACE_BOUND ( 'NONE', #5528, .T. ) ;
#2395=FACE_BOUND ( 'NONE', #17737, .T. ) ;
#2405=SURFACE_STYLE_USAGE ( .BOTH. , #13249 ) ;
#2447=VECTOR ( 'NONE', #16824, 1000.000000000000000 ) ;
#2465=CARTESIAN_POINT ( 'NONE',  ( 78.48937290013660117, 113.1299228374914208, 170.4174721992565082 ) ) ;
#2483=VERTEX_POINT ( 'NONE', #2581 ) ;
#2488=SURFACE_STYLE_USAGE ( .BOTH. , #13332 ) ;
#2490=DIRECTION ( 'NONE',  ( 1.000000000000000000, 9.815121534730717399E-17, -0.000000000000000000 ) ) ;
#2491=FACE_OUTER_BOUND ( 'NONE', #3037, .T. ) ;
#2494=DIRECTION ( 'NONE',  ( -1.000000000000000000, 0.000000000000000000, 0.000000000000000000 ) ) ;
#2498=ORIENTED_EDGE ( 'NONE', *, *, #8382, .T. ) ;
#2502=ADVANCED_BREP_SHAPE_REPRESENTATION ( '', ( #1368, #1329, #1516, #2741 ), #5722 ) ;
#2503=CARTESIAN_POINT ( 'NONE',  ( 153.4893729001366580, 80.91625508013694912, 250.0000000000000000 ) ) ;
#2510=VECTOR ( 'NONE', #6917, 1000.000000000000000 ) ;
#2518=( NAMED_UNIT ( * ) SI_UNIT ( $, .STERADIAN. ) SOLID_ANGLE_UNIT ( ) );
#2519=CARTESIAN_POINT ( 'NONE',  ( 153.4893729001366864, 123.1299228374914634, 79.58252780074349175 ) ) ;
#2542=FILL_AREA_STYLE_COLOUR ( '', #6913 ) ;
#2553=CARTESIAN_POINT ( 'NONE',  ( 178.4893729001365728, 103.1299228374914776, 29.36128450348865471 ) ) ;
#2558=CARTESIAN_POINT ( 'NONE',  ( 153.4893729001366864, 113.1299228374914634, 170.4174721992565082 ) ) ;
#2574=EDGE_LOOP ( 'NONE', ( #1496, #6237, #15794, #7280 ) ) ;
#2579=SURFACE_STYLE_USAGE ( .BOTH. , #11774 ) ;
#2581=CARTESIAN_POINT ( 'NONE',  ( 98.48937290013662960, 103.1299228374914208, 79.58252780074349175 ) ) ;
#2582=DIRECTION ( 'NONE',  ( 0.000000000000000000, 1.000000000000000000, 0.000000000000000000 ) ) ;
#2590=STYLED_ITEM ( 'NONE', ( #19408 ), #11064 ) ;
#2592=DIRECTION ( 'NONE',  ( -0.000000000000000000, 0.000000000000000000, 1.000000000000000000 ) ) ;
#2603=EDGE_LOOP ( 'NONE', ( #6537, #8500, #14463, #17208, #1300, #7777, #11421, #14190 ) ) ;
#2613=FACE_OUTER_BOUND ( 'NONE', #17692, .T. ) ;
#2615=( NAMED_UNIT ( * ) PLANE_ANGLE_UNIT ( ) SI_UNIT ( $, .RADIAN. ) );
#2619=ORIENTED_EDGE ( 'NONE', *, *, #17461, .T. ) ;
#2622=ORIENTED_EDGE ( 'NONE', *, *, #12264, .T. ) ;
#2625=DIRECTION ( 'NONE',  ( 1.000000000000000000, 5.889072920838430686E-16, -0.000000000000000000 ) ) ;
#2629=DIRECTION ( 'NONE',  ( -1.000000000000000000, -2.135044278125301096E-16, -0.000000000000000000 ) ) ;
#2654=( LENGTH_UNIT ( ) NAMED_UNIT ( * ) SI_UNIT ( .MILLI., .METRE. ) );
#2655=CARTESIAN_POINT ( 'NONE',  ( -0.000000000000000000, 167.9162550801369491, 250.0000000000000000 ) ) ;
#2661=MECHANICAL_DESIGN_GEOMETRIC_PRESENTATION_REPRESENTATION('',(#27),#13859);
#2664=LINE ( 'NONE', #18423, #9988 ) ;
#2677=LINE ( 'NONE', #2878, #10726 ) ;
#2701=SURFACE_SIDE_STYLE ('',( #10542 ) ) ;
#2702=UNCERTAINTY_MEASURE_WITH_UNIT (LENGTH_MEASURE( 1.000000000000000082E-05 ), #7069, 'distance_accuracy_value', 'NONE');
#2705=SURFACE_STYLE_USAGE ( .BOTH. , #16843 ) ;
#2711=( NAMED_UNIT ( * ) PLANE_ANGLE_UNIT ( ) SI_UNIT ( $, .RADIAN. ) );
#2714=SURFACE_STYLE_FILL_AREA ( #13748 ) ;
#2717=SURFACE_STYLE_FILL_AREA ( #16762 ) ;
#2733=DIRECTION ( 'NONE',  ( 0.000000000000000000, -1.000000000000000000, 0.000000000000000000 ) ) ;
#2738=LINE ( 'NONE', #8739, #3421 ) ;
#2741=AXIS2_PLACEMENT_3D ( 'NONE', #5042, #3500, #8234 ) ;
#2745=DIRECTION ( 'NONE',  ( 0.000000000000000000, 0.000000000000000000, 1.000000000000000000 ) ) ;
#2746=( NAMED_UNIT ( * ) SI_UNIT ( $, .STERADIAN. ) SOLID_ANGLE_UNIT ( ) );
#2752=ORIENTED_EDGE ( 'NONE', *, *, #1627, .T. ) ;
#2756=FILL_AREA_STYLE ('',( #1383 ) ) ;
#2757=MECHANICAL_DESIGN_GEOMETRIC_PRESENTATION_REPRESENTATION('',(#15962),#1428);
#2761=ORIENTED_EDGE ( 'NONE', *, *, #9735, .F. ) ;
#2766=PRESENTATION_STYLE_ASSIGNMENT (( #17090 ) ) ;
#2776=ORIENTED_EDGE ( 'NONE', *, *, #1175, .F. ) ;
#2785=FACE_OUTER_BOUND ( 'NONE', #13609, .T. ) ;
#2790=CARTESIAN_POINT ( 'NONE',  ( 178.4893729001365443, 167.9162550801369491, 0.000000000000000000 ) ) ;
#2802=ORIENTED_EDGE ( 'NONE', *, *, #18707, .F. ) ;
#2805=( NAMED_UNIT ( * ) SI_UNIT ( $, .STERADIAN. ) SOLID_ANGLE_UNIT ( ) );
#2823=ORIENTED_EDGE ( 'NONE', *, *, #20202, .F. ) ;
#2831=LINE ( 'NONE', #4198, #13963 ) ;
#2832=EDGE_LOOP ( 'NONE', ( #171, #19097 ) ) ;
#2837=CYLINDRICAL_SURFACE ( 'NONE', #12259, 10.00000000000000888 ) ;
#2857=EDGE_LOOP ( 'NONE', ( #1695, #3174 ) ) ;
#2861=DIRECTION ( 'NONE',  ( 0.000000000000000000, 0.000000000000000000, -1.000000000000000000 ) ) ;
#2866=PLANE ( 'NONE',  #18760 ) ;
#2874=VERTEX_POINT ( 'NONE', #8943 ) ;
#2876=VERTEX_POINT ( 'NONE', #2959 ) ;
#2877=VERTEX_POINT ( 'NONE', #19859 ) ;
#2878=CARTESIAN_POINT ( 'NONE',  ( 178.4893729001365443, 0.000000000000000000, 0.000000000000000000 ) ) ;
#2883=SURFACE_SIDE_STYLE ('',( #9480 ) ) ;
#2885=( NAMED_UNIT ( * ) PLANE_ANGLE_UNIT ( ) SI_UNIT ( $, .RADIAN. ) );
#2888=LINE ( 'NONE', #19673, #10028 ) ;
#2897=ADVANCED_FACE ( 'NONE', ( #15360 ), #14006, .F. ) ;
#2900=( NAMED_UNIT ( * ) SI_UNIT ( $, .STERADIAN. ) SOLID_ANGLE_UNIT ( ) );
#2903=CARTESIAN_POINT ( 'NONE',  ( -211.5106270998635409, 113.1299228374912502, 29.36128450348865471 ) ) ;
#2910=SURFACE_STYLE_FILL_AREA ( #17349 ) ;
#2924=ADVANCED_FACE ( 'NONE', ( #15247 ), #16902, .F. ) ;
#2930=( GEOMETRIC_REPRESENTATION_CONTEXT ( 3 ) GLOBAL_UNCERTAINTY_ASSIGNED_CONTEXT ( ( #2049 ) ) GLOBAL_UNIT_ASSIGNED_CONTEXT ( ( #5162, #11741, #3901 ) ) REPRESENTATION_CONTEXT ( 'NONE', 'WORKASPACE' ) );
#2931=CARTESIAN_POINT ( 'NONE',  ( 133.4893729001365443, 123.1299228374914634, 29.36128450348865471 ) ) ;
#2932=DIRECTION ( 'NONE',  ( -5.889072920838430686E-16, 1.000000000000000000, -0.000000000000000000 ) ) ;
#2942=DIRECTION ( 'NONE',  ( 0.000000000000000000, 1.000000000000000000, -0.000000000000000000 ) ) ;
#2958=EDGE_LOOP ( 'NONE', ( #5308, #618 ) ) ;
#2959=CARTESIAN_POINT ( 'NONE',  ( 153.4893729001366864, 103.1299228374914492, 170.4174721992565082 ) ) ;
#2961=EDGE_CURVE ( 'NONE', #2483, #1058, #7980, .T. ) ;
#2967=AXIS2_PLACEMENT_3D ( 'NONE', #4443, #10730, #17024 ) ;
#2971=EDGE_CURVE ( 'NONE', #198, #20118, #3278, .T. ) ;
#2976=CARTESIAN_POINT ( 'NONE',  ( 133.4893729001365728, 80.91625508013694912, -97.94896630388704750 ) ) ;
#2977=EDGE_LOOP ( 'NONE', ( #9265, #3920 ) ) ;
#2983=AXIS2_PLACEMENT_3D ( 'NONE', #4776, #11056, #17334 ) ;
#2984=SURFACE_STYLE_USAGE ( .BOTH. , #17103 ) ;
#2988=( LENGTH_UNIT ( ) NAMED_UNIT ( * ) SI_UNIT ( .MILLI., .METRE. ) );
#2992=EDGE_LOOP ( 'NONE', ( #15930, #11221, #8173, #11413 ) ) ;
#2994=( GEOMETRIC_REPRESENTATION_CONTEXT ( 3 ) GLOBAL_UNCERTAINTY_ASSIGNED_CONTEXT ( ( #16333 ) ) GLOBAL_UNIT_ASSIGNED_CONTEXT ( ( #6563, #17574, #16064 ) ) REPRESENTATION_CONTEXT ( 'NONE', 'WORKASPACE' ) );
#3002=FILL_AREA_STYLE ('',( #3316 ) ) ;
#3009=VECTOR ( 'NONE', #8827, 1000.000000000000000 ) ;
#3011=DIRECTION ( 'NONE',  ( 1.000000000000000000, 5.889072920838430686E-16, 0.000000000000000000 ) ) ;
#3013=DIRECTION ( 'NONE',  ( 1.000000000000000000, 5.889072920838430686E-16, -0.000000000000000000 ) ) ;
#3020=ORIENTED_EDGE ( 'NONE', *, *, #11532, .T. ) ;
#3037=EDGE_LOOP ( 'NONE', ( #5651, #1146, #2823, #20124 ) ) ;
#3041=DIRECTION ( 'NONE',  ( 0.000000000000000000, 1.000000000000000000, -0.000000000000000000 ) ) ;
#3044=PRODUCT_DEFINITION_FORMATION_WITH_SPECIFIED_SOURCE ( 'ANY', '', #11412, .NOT_KNOWN. ) ;
#3053=ORIENTED_EDGE ( 'NONE', *, *, #15093, .F. ) ;
#3072=DIRECTION ( 'NONE',  ( -1.000000000000000000, -0.000000000000000000, -0.000000000000000000 ) ) ;
#3080=VECTOR ( 'NONE', #1731, 1000.000000000000000 ) ;
#3084=EDGE_CURVE ( 'NONE', #12290, #8120, #5536, .T. ) ;
#3093=VERTEX_POINT ( 'NONE', #2128 ) ;
#3102=LINE ( 'NONE', #4758, #12624 ) ;
#3122=( LENGTH_UNIT ( ) NAMED_UNIT ( * ) SI_UNIT ( .MILLI., .METRE. ) );
#3123=LINE ( 'NONE', #15718, #15147 ) ;
#3125=ORIENTED_EDGE ( 'NONE', *, *, #19252, .T. ) ;
#3152=FACE_BOUND ( 'NONE', #18412, .T. ) ;
#3174=ORIENTED_EDGE ( 'NONE', *, *, #13775, .F. ) ;
#3179=COLOUR_RGB ( '', 0.31764706, 0.68627451, 0.89019608) ;
#3193=UNCERTAINTY_MEASURE_WITH_UNIT (LENGTH_MEASURE( 1.000000000000000082E-05 ), #8681, 'distance_accuracy_value', 'NONE');
#3199=CARTESIAN_POINT ( 'NONE',  ( 178.4893729001365443, 167.9162550801369491, -97.94896630388704750 ) ) ;
#3205=VECTOR ( 'NONE', #14949, 1000.000000000000000 ) ;
#3217=LINE ( 'NONE', #8174, #8573 ) ;
#3219=EDGE_CURVE ( 'NONE', #5436, #1247, #13479, .T. ) ;
#3222=ORIENTED_EDGE ( 'NONE', *, *, #7227, .T. ) ;
#3236=VERTEX_POINT ( 'NONE', #18610 ) ;
#3246=LINE ( 'NONE', #6661, #7711 ) ;
#3249=DIRECTION ( 'NONE',  ( 1.000000000000000000, 2.135044278125300850E-16, -0.000000000000000000 ) ) ;
#3258=CARTESIAN_POINT ( 'NONE',  ( 178.4893729001365728, 113.1299228374914918, 170.4174721992565082 ) ) ;
#3276=ORIENTED_EDGE ( 'NONE', *, *, #12264, .F. ) ;
#3278=LINE ( 'NONE', #4622, #19800 ) ;
#3285=CARTESIAN_POINT ( 'NONE',  ( 133.4893729001365443, 113.1299228374914634, 220.6387154965113382 ) ) ;
#3288=COLOUR_RGB ( '', 0.31764706, 0.68627451, 0.89019608) ;
#3292=ORIENTED_EDGE ( 'NONE', *, *, #1175, .T. ) ;
#3293=ORIENTED_EDGE ( 'NONE', *, *, #16438, .T. ) ;
#3296=CARTESIAN_POINT ( 'NONE',  ( 53.48937290013658696, 123.1299228374914065, 170.4174721992565082 ) ) ;
#3301=VECTOR ( 'NONE', #8761, 1000.000000000000000 ) ;
#3302=VERTEX_POINT ( 'NONE', #2931 ) ;
#3310=MECHANICAL_DESIGN_GEOMETRIC_PRESENTATION_REPRESENTATION('',(#3659),#14829);
#3315=ORIENTED_EDGE ( 'NONE', *, *, #10147, .F. ) ;
#3316=FILL_AREA_STYLE_COLOUR ( '', #16299 ) ;
#3321=ADVANCED_FACE ( 'NONE', ( #16873 ), #2837, .F. ) ;
#3342=AXIS2_PLACEMENT_3D ( 'NONE', #2307, #17780, #5227 ) ;
#3348=CARTESIAN_POINT ( 'NONE',  ( -211.5106270998635409, 103.1299228374912360, 220.6387154965113382 ) ) ;
#3350=CARTESIAN_POINT ( 'NONE',  ( 98.48937290013662960, 123.1299228374914350, 79.58252780074349175 ) ) ;
#3356=( NAMED_UNIT ( * ) PLANE_ANGLE_UNIT ( ) SI_UNIT ( $, .RADIAN. ) );
#3374=CIRCLE ( 'NONE', #14891, 10.00000000000000888 ) ;
#3385=LINE ( 'NONE', #9973, #14942 ) ;
#3404=ORIENTED_EDGE ( 'NONE', *, *, #8914, .F. ) ;
#3411=PRESENTATION_STYLE_ASSIGNMENT (( #1937 ) ) ;
#3421=VECTOR ( 'NONE', #779, 1000.000000000000000 ) ;
#3426=SURFACE_STYLE_USAGE ( .BOTH. , #6428 ) ;
#3444=DIRECTION ( 'NONE',  ( 1.000000000000000000, -0.000000000000000000, 0.000000000000000000 ) ) ;
#3445=EDGE_CURVE ( 'NONE', #5831, #10467, #4902, .T. ) ;
#3446=EDGE_LOOP ( 'NONE', ( #20105, #7303, #18238, #2213, #14566, #19545 ) ) ;
#3452=EDGE_CURVE ( 'NONE', #15858, #6545, #8789, .T. ) ;
#3456=ORIENTED_EDGE ( 'NONE', *, *, #12594, .F. ) ;
#3468=CARTESIAN_POINT ( 'NONE',  ( 53.48937290013659407, 145.9162550801369491, 250.0000000000000000 ) ) ;
#3470=DIRECTION ( 'NONE',  ( 1.000000000000000000, 5.889072920838430686E-16, -0.000000000000000000 ) ) ;
#3474=ORIENTED_EDGE ( 'NONE', *, *, #18592, .T. ) ;
#3476=FILL_AREA_STYLE_COLOUR ( '', #12893 ) ;
#3478=MECHANICAL_DESIGN_GEOMETRIC_PRESENTATION_REPRESENTATION('',(#823),#13665);
#3485=EDGE_LOOP ( 'NONE', ( #1245, #14570 ) ) ;
#3497=( LENGTH_UNIT ( ) NAMED_UNIT ( * ) SI_UNIT ( .MILLI., .METRE. ) );
#3500=DIRECTION ( 'NONE',  ( 0.000000000000000000, 0.000000000000000000, 1.000000000000000000 ) ) ;
#3504=CARTESIAN_POINT ( 'NONE',  ( 53.48937290013659407, 145.9162550801369491, 250.0000000000000000 ) ) ;
#3513=CARTESIAN_POINT ( 'NONE',  ( 178.4893729001365443, 145.9162550801369491, 250.0000000000000000 ) ) ;
#3518=EDGE_CURVE ( 'NONE', #19410, #7140, #10293, .T. ) ;
#3520=CARTESIAN_POINT ( 'NONE',  ( 149.0892156028631348, 80.91625508013694912, 250.0000000000000000 ) ) ;
#3534=ORIENTED_EDGE ( 'NONE', *, *, #49, .T. ) ;
#3535=CARTESIAN_POINT ( 'NONE',  ( 133.4893729001365443, 103.1299228374914492, 29.36128450348865471 ) ) ;
#3543=DIRECTION ( 'NONE',  ( 1.000000000000000000, 0.000000000000000000, 0.000000000000000000 ) ) ;
#3560=SURFACE_STYLE_FILL_AREA ( #2191 ) ;
#3588=DIRECTION ( 'NONE',  ( 0.000000000000000000, -1.000000000000000000, 0.000000000000000000 ) ) ;
#3589=VERTEX_POINT ( 'NONE', #15593 ) ;
#3593=MECHANICAL_DESIGN_GEOMETRIC_PRESENTATION_REPRESENTATION('',(#20352),#17732);
#3603=CYLINDRICAL_SURFACE ( 'NONE', #19705, 10.00000000000000888 ) ;
#3607=MECHANICAL_DESIGN_GEOMETRIC_PRESENTATION_REPRESENTATION('',(#5612),#7581);
#3615=DIRECTION ( 'NONE',  ( 0.000000000000000000, -1.000000000000000000, 0.000000000000000000 ) ) ;
#3617=PLANE ( 'NONE',  #4728 ) ;
#3627=EDGE_CURVE ( 'NONE', #16599, #1681, #17215, .T. ) ;
#3630=ORIENTED_EDGE ( 'NONE', *, *, #6654, .F. ) ;
#3634=FILL_AREA_STYLE_COLOUR ( '', #6300 ) ;
#3638=VERTEX_POINT ( 'NONE', #2790 ) ;
#3640=CARTESIAN_POINT ( 'NONE',  ( 178.4893729001365728, 113.1299228374914918, 220.6387154965113382 ) ) ;
#3641=SURFACE_SIDE_STYLE ('',( #3849 ) ) ;
#3643=FACE_OUTER_BOUND ( 'NONE', #6297, .T. ) ;
#3645=( NAMED_UNIT ( * ) SI_UNIT ( $, .STERADIAN. ) SOLID_ANGLE_UNIT ( ) );
#3659=STYLED_ITEM ( 'NONE', ( #6139 ), #16856 ) ;
#3661=ORIENTED_EDGE ( 'NONE', *, *, #923, .F. ) ;
#3664=PRESENTATION_STYLE_ASSIGNMENT (( #5417 ) ) ;
#3670=( NAMED_UNIT ( * ) SI_UNIT ( $, .STERADIAN. ) SOLID_ANGLE_UNIT ( ) );
#3672=VERTEX_POINT ( 'NONE', #12389 ) ;
#3675=VECTOR ( 'NONE', #13616, 1000.000000000000000 ) ;
#3676=EDGE_LOOP ( 'NONE', ( #19396, #18917, #10092, #1296 ) ) ;
#3692=CARTESIAN_POINT ( 'NONE',  ( -211.5106270998635409, 123.1299228374912644, 170.4174721992565082 ) ) ;
#3708=LINE ( 'NONE', #5652, #2510 ) ;
#3713=CARTESIAN_POINT ( 'NONE',  ( 78.48937290013660117, 123.1299228374914208, 29.36128450348865471 ) ) ;
#3717=CARTESIAN_POINT ( 'NONE',  ( 78.48937290013660117, 103.1299228374914065, 170.4174721992565082 ) ) ;
#3737=CARTESIAN_POINT ( 'NONE',  ( 0.000000000000000000, 0.000000000000000000, 0.000000000000000000 ) ) ;
#3762=( LENGTH_UNIT ( ) NAMED_UNIT ( * ) SI_UNIT ( .MILLI., .METRE. ) );
#3768=AXIS2_PLACEMENT_3D ( 'NONE', #16742, #2592, #18557 ) ;
#3774=PRESENTATION_STYLE_ASSIGNMENT (( #11593 ) ) ;
#3780=CIRCLE ( 'NONE', #472, 10.00000000000000888 ) ;
#3783=ORIENTED_EDGE ( 'NONE', *, *, #1418, .T. ) ;
#3840=ORIENTED_EDGE ( 'NONE', *, *, #8136, .T. ) ;
#3849=SURFACE_STYLE_FILL_AREA ( #14668 ) ;
#3857=EDGE_CURVE ( 'NONE', #11725, #2115, #18022, .T. ) ;
#3859=ORIENTED_EDGE ( 'NONE', *, *, #847, .F. ) ;
#3862=( NAMED_UNIT ( * ) PLANE_ANGLE_UNIT ( ) SI_UNIT ( $, .RADIAN. ) );
#3869=CYLINDRICAL_SURFACE ( 'NONE', #17935, 10.00000000000000888 ) ;
#3871=CARTESIAN_POINT ( 'NONE',  ( 133.4893729001365443, 113.1299228374914634, 220.6387154965113382 ) ) ;
#3880=ORIENTED_EDGE ( 'NONE', *, *, #7969, .F. ) ;
#3886=VERTEX_POINT ( 'NONE', #8766 ) ;
#3900=CIRCLE ( 'NONE', #5873, 10.00000000000000888 ) ;
#3901=( NAMED_UNIT ( * ) SI_UNIT ( $, .STERADIAN. ) SOLID_ANGLE_UNIT ( ) );
#3903=EDGE_CURVE ( 'NONE', #11436, #9454, #813, .T. ) ;
#3920=ORIENTED_EDGE ( 'NONE', *, *, #18599, .T. ) ;
#3926=VERTEX_POINT ( 'NONE', #3717 ) ;
#3927=DIRECTION ( 'NONE',  ( 1.000000000000000000, 5.889072920838430686E-16, -0.000000000000000000 ) ) ;
#3931=FILL_AREA_STYLE ('',( #15065 ) ) ;
#3932=CIRCLE ( 'NONE', #12493, 10.00000000000000888 ) ;
#3934=SHAPE_REPRESENTATION ( 'Part10^Assem2', ( #2741 ), #5722 ) ;
#3951=EDGE_LOOP ( 'NONE', ( #1413, #4610 ) ) ;
#3957=EDGE_CURVE ( 'NONE', #10947, #243, #15047, .T. ) ;
#3961=COLOUR_RGB ( '', 0.08235294, 0.09019608, 0.10196078) ;
#3965=STYLED_ITEM ( 'NONE', ( #12384 ), #6282 ) ;
#3970=DIRECTION ( 'NONE',  ( 1.000000000000000000, 9.815121534730717399E-17, -0.000000000000000000 ) ) ;
#3978=( GEOMETRIC_REPRESENTATION_CONTEXT ( 3 ) GLOBAL_UNCERTAINTY_ASSIGNED_CONTEXT ( ( #1023 ) ) GLOBAL_UNIT_ASSIGNED_CONTEXT ( ( #15714, #8270, #17642 ) ) REPRESENTATION_CONTEXT ( 'NONE', 'WORKASPACE' ) );
#4015=( NAMED_UNIT ( * ) PLANE_ANGLE_UNIT ( ) SI_UNIT ( $, .RADIAN. ) );
#4022=EDGE_LOOP ( 'NONE', ( #10564, #16560, #11147, #12078 ) ) ;
#4026=CARTESIAN_POINT ( 'NONE',  ( 178.4893729001365728, 113.1299228374914918, 29.36128450348865471 ) ) ;
#4035=DIRECTION ( 'NONE',  ( 0.000000000000000000, 1.000000000000000000, 0.000000000000000000 ) ) ;
#4038=EDGE_CURVE ( 'NONE', #4273, #15658, #12103, .T. ) ;
#4040=VECTOR ( 'NONE', #9945, 1000.000000000000000 ) ;
#4046=VECTOR ( 'NONE', #3470, 1000.000000000000000 ) ;
#4057=CIRCLE ( 'NONE', #19833, 10.00000000000000888 ) ;
#4059=CARTESIAN_POINT ( 'NONE',  ( 133.4893729001365443, 123.1299228374914634, 79.58252780074349175 ) ) ;
#4063=LINE ( 'NONE', #4181, #12271 ) ;
#4065=STYLED_ITEM ( 'NONE', ( #3411 ), #14169 ) ;
#4066=STYLED_ITEM ( 'NONE', ( #5714 ), #18929 ) ;
#4073=PLANE ( 'NONE',  #280 ) ;
#4079=FACE_OUTER_BOUND ( 'NONE', #13664, .T. ) ;
#4108=EDGE_CURVE ( 'NONE', #8200, #16217, #14200, .T. ) ;
#4156=DIRECTION ( 'NONE',  ( 1.000000000000000000, 5.889072920838430686E-16, -0.000000000000000000 ) ) ;
#4165=ORIENTED_EDGE ( 'NONE', *, *, #19544, .T. ) ;
#4181=CARTESIAN_POINT ( 'NONE',  ( -211.5106270998635409, 103.1299228374912360, 79.58252780074349175 ) ) ;
#4187=CARTESIAN_POINT ( 'NONE',  ( 82.88953019741013861, 167.9162550801369491, 245.0000000000000000 ) ) ;
#4189=EDGE_LOOP ( 'NONE', ( #19742, #5236, #3125, #12932 ) ) ;
#4193=ORIENTED_EDGE ( 'NONE', *, *, #20202, .T. ) ;
#4195=EDGE_CURVE ( 'NONE', #2876, #13587, #11791, .T. ) ;
#4198=CARTESIAN_POINT ( 'NONE',  ( -211.5106270998635409, 123.1299228374912644, 170.4174721992565082 ) ) ;
#4215=LINE ( 'NONE', #12653, #18918 ) ;
#4230=DIRECTION ( 'NONE',  ( 1.000000000000000000, 9.815121534730717399E-17, -0.000000000000000000 ) ) ;
#4236=EDGE_CURVE ( 'NONE', #20287, #4620, #12780, .T. ) ;
#4237=ORIENTED_EDGE ( 'NONE', *, *, #10751, .T. ) ;
#4238=EDGE_CURVE ( 'NONE', #13587, #19445, #780, .T. ) ;
#4239=( GEOMETRIC_REPRESENTATION_CONTEXT ( 3 ) GLOBAL_UNCERTAINTY_ASSIGNED_CONTEXT ( ( #6865 ) ) GLOBAL_UNIT_ASSIGNED_CONTEXT ( ( #2202, #5615, #2518 ) ) REPRESENTATION_CONTEXT ( 'NONE', 'WORKASPACE' ) );
#4246=DIRECTION ( 'NONE',  ( 1.000000000000000000, 0.000000000000000000, 0.000000000000000000 ) ) ;
#4251=FACE_OUTER_BOUND ( 'NONE', #1514, .T. ) ;
#4255=PRESENTATION_STYLE_ASSIGNMENT (( #1315 ) ) ;
#4258=STYLED_ITEM ( 'NONE', ( #2139 ), #16193 ) ;
#4265=FILL_AREA_STYLE ('',( #18361 ) ) ;
#4268=( NAMED_UNIT ( * ) PLANE_ANGLE_UNIT ( ) SI_UNIT ( $, .RADIAN. ) );
#4273=VERTEX_POINT ( 'NONE', #6808 ) ;
#4274=DIRECTION ( 'NONE',  ( 0.000000000000000000, 1.000000000000000000, 0.000000000000000000 ) ) ;
#4293=FACE_BOUND ( 'NONE', #11841, .T. ) ;
#4303=( GEOMETRIC_REPRESENTATION_CONTEXT ( 3 ) GLOBAL_UNCERTAINTY_ASSIGNED_CONTEXT ( ( #19790 ) ) GLOBAL_UNIT_ASSIGNED_CONTEXT ( ( #13701, #18414, #12237 ) ) REPRESENTATION_CONTEXT ( 'NONE', 'WORKASPACE' ) );
#4308=EDGE_CURVE ( 'NONE', #19266, #6461, #19342, .T. ) ;
#4309=DIRECTION ( 'NONE',  ( 2.135044278125301096E-16, -1.000000000000000000, 0.000000000000000000 ) ) ;
#4321=FILL_AREA_STYLE ('',( #991 ) ) ;
#4338=CARTESIAN_POINT ( 'NONE',  ( 78.48937290013661539, 80.91625508013694912, -97.94896630388704750 ) ) ;
#4356=CIRCLE ( 'NONE', #9967, 10.00000000000000888 ) ;
#4360=LINE ( 'NONE', #17235, #13686 ) ;
#4371=VERTEX_POINT ( 'NONE', #19726 ) ;
#4377=VECTOR ( 'NONE', #9797, 1000.000000000000000 ) ;
#4391=STYLED_ITEM ( 'NONE', ( #2766 ), #20192 ) ;
#4398=DIRECTION ( 'NONE',  ( -1.000000000000000000, 0.000000000000000000, 0.000000000000000000 ) ) ;
#4408=EDGE_LOOP ( 'NONE', ( #8864, #15371 ) ) ;
#4410=ORIENTED_EDGE ( 'NONE', *, *, #7619, .T. ) ;
#4420=PRESENTATION_STYLE_ASSIGNMENT (( #8945 ) ) ;
#4423=SURFACE_SIDE_STYLE ('',( #15145 ) ) ;
#4427=COLOUR_RGB ( '', 0.09019608, 0.27058824, 0.51372549) ;
#4443=CARTESIAN_POINT ( 'NONE',  ( 53.48937290013659407, 0.000000000000000000, -97.94896630388704750 ) ) ;
#4446=CARTESIAN_POINT ( 'NONE',  ( 53.48937290013660828, 34.32473510485366575, -140.0000000000001137 ) ) ;
#4450=VECTOR ( 'NONE', #17376, 1000.000000000000000 ) ;
#4463=CARTESIAN_POINT ( 'NONE',  ( 153.4893729001366864, 113.1299228374914634, 220.6387154965113382 ) ) ;
#4469=( NAMED_UNIT ( * ) SI_UNIT ( $, .STERADIAN. ) SOLID_ANGLE_UNIT ( ) );
#4471=CARTESIAN_POINT ( 'NONE',  ( 98.48937290013662960, 103.1299228374914208, 220.6387154965113382 ) ) ;
#4475=EDGE_CURVE ( 'NONE', #14026, #20287, #4602, .T. ) ;
#4481=SURFACE_STYLE_USAGE ( .BOTH. , #18473 ) ;
#4492=DIRECTION ( 'NONE',  ( 1.000000000000000000, -0.000000000000000000, 0.000000000000000000 ) ) ;
#4493=EDGE_CURVE ( 'NONE', #18122, #17418, #3900, .T. ) ;
#4494=EDGE_LOOP ( 'NONE', ( #13326, #4721, #4743, #15683 ) ) ;
#4498=DIRECTION ( 'NONE',  ( 0.000000000000000000, 1.000000000000000000, 0.000000000000000000 ) ) ;
#4531=PRESENTATION_STYLE_ASSIGNMENT (( #12753 ) ) ;
#4540=AXIS2_PLACEMENT_3D ( 'NONE', #6437, #17433, #14141 ) ;
#4542=CARTESIAN_POINT ( 'NONE',  ( 78.48937290013662960, 1.675782865040797740E-14, 250.0000000000000000 ) ) ;
#4543=FILL_AREA_STYLE ('',( #17022 ) ) ;
#4544=VECTOR ( 'NONE', #11832, 1000.000000000000000 ) ;
#4547=ORIENTED_EDGE ( 'NONE', *, *, #6681, .T. ) ;
#4564=ORIENTED_EDGE ( 'NONE', *, *, #1601, .F. ) ;
#4566=FILL_AREA_STYLE_COLOUR ( '', #5079 ) ;
#4578=EDGE_LOOP ( 'NONE', ( #7378, #18866, #4237, #11123, #18970, #1786, #15726, #13323 ) ) ;
#4580=ORIENTED_EDGE ( 'NONE', *, *, #9385, .F. ) ;
#4583=EDGE_CURVE ( 'NONE', #17875, #10467, #19009, .T. ) ;
#4586=LINE ( 'NONE', #7879, #513 ) ;
#4587=ORIENTED_EDGE ( 'NONE', *, *, #1002, .F. ) ;
#4590=CARTESIAN_POINT ( 'NONE',  ( 0.000000000000000000, 145.9162550801369491, 0.000000000000000000 ) ) ;
#4596=DIRECTION ( 'NONE',  ( 1.000000000000000000, 0.000000000000000000, 0.000000000000000000 ) ) ;
#4602=LINE ( 'NONE', #18497, #1554 ) ;
#4610=ORIENTED_EDGE ( 'NONE', *, *, #6494, .T. ) ;
#4612=VERTEX_POINT ( 'NONE', #10988 ) ;
#4615=SURFACE_STYLE_USAGE ( .BOTH. , #16791 ) ;
#4617=EDGE_CURVE ( 'NONE', #1665, #14262, #4814, .T. ) ;
#4620=VERTEX_POINT ( 'NONE', #12962 ) ;
#4622=CARTESIAN_POINT ( 'NONE',  ( -0.000000000000000000, 167.9162550801369491, 250.0000000000000000 ) ) ;
#4644=MECHANICAL_DESIGN_GEOMETRIC_PRESENTATION_REPRESENTATION('',(#15509),#4303);
#4664=SURFACE_STYLE_USAGE ( .BOTH. , #7559 ) ;
#4678=EDGE_LOOP ( 'NONE', ( #13803, #8584, #11165, #5437 ) ) ;
#4687=VERTEX_POINT ( 'NONE', #10150 ) ;
#4697=EDGE_LOOP ( 'NONE', ( #7228, #4928, #14993, #2776 ) ) ;
#4710=AXIS2_PLACEMENT_3D ( 'NONE', #724, #14449, #19382 ) ;
#4716=DIRECTION ( 'NONE',  ( 1.000000000000000000, 0.000000000000000000, 0.000000000000000000 ) ) ;
#4719=CLOSED_SHELL ( 'NONE', ( #17786, #12124, #7362, #16227, #14509, #14853, #11393, #6214, #16193, #10903, #18929, #11917, #18911, #1321, #9624, #14169, #6993, #14002, #5022, #192, #7251, #343, #20192, #3321, #19322, #7501 ) ) ;
#4721=ORIENTED_EDGE ( 'NONE', *, *, #20310, .F. ) ;
#4723=DIRECTION ( 'NONE',  ( -1.000000000000000000, -1.595148023886719315E-16, 0.000000000000000000 ) ) ;
#4728=AXIS2_PLACEMENT_3D ( 'NONE', #19360, #4596, #13979 ) ;
#4743=ORIENTED_EDGE ( 'NONE', *, *, #19777, .T. ) ;
#4748=AXIS2_PLACEMENT_3D ( 'NONE', #5402, #5502, #17756 ) ;
#4757=MECHANICAL_DESIGN_GEOMETRIC_PRESENTATION_REPRESENTATION('',(#11000),#12655);
#4758=CARTESIAN_POINT ( 'NONE',  ( 82.88953019741013861, 80.91625508013694912, 250.0000000000000000 ) ) ;
#4773=VECTOR ( 'NONE', #20183, 1000.000000000000000 ) ;
#4776=CARTESIAN_POINT ( 'NONE',  ( -211.5106270998635409, 113.1299228374912502, 220.6387154965113382 ) ) ;
#4791=DIRECTION ( 'NONE',  ( -0.000000000000000000, 0.000000000000000000, 1.000000000000000000 ) ) ;
#4794=ORIENTED_EDGE ( 'NONE', *, *, #11378, .F. ) ;
#4801=STYLED_ITEM ( 'NONE', ( #13435 ), #2347 ) ;
#4811=SURFACE_SIDE_STYLE ('',( #12531 ) ) ;
#4814=LINE ( 'NONE', #12642, #16417 ) ;
#4829=ORIENTED_EDGE ( 'NONE', *, *, #7116, .F. ) ;
#4833=ADVANCED_FACE ( 'NONE', ( #9951 ), #13159, .F. ) ;
#4856=ADVANCED_FACE ( 'NONE', ( #2613 ), #4073, .T. ) ;
#4857=FILL_AREA_STYLE_COLOUR ( '', #12866 ) ;
#4861=DIRECTION ( 'NONE',  ( 1.000000000000000000, -0.000000000000000000, 0.000000000000000000 ) ) ;
#4868=ADVANCED_FACE ( 'NONE', ( #12105 ), #1234, .F. ) ;
#4877=DIRECTION ( 'NONE',  ( 0.000000000000000000, 1.000000000000000000, 0.000000000000000000 ) ) ;
#4885=PLANE ( 'NONE',  #16607 ) ;
#4891=ORIENTED_EDGE ( 'NONE', *, *, #7607, .F. ) ;
#4897=CARTESIAN_POINT ( 'NONE',  ( 98.48937290013662960, 113.1299228374914350, 220.6387154965113382 ) ) ;
#4901=PLANE ( 'NONE',  #7907 ) ;
#4902=LINE ( 'NONE', #17565, #4046 ) ;
#4906=CARTESIAN_POINT ( 'NONE',  ( 98.48937290013662960, 113.1299228374914350, 170.4174721992565082 ) ) ;
#4908=LINE ( 'NONE', #18802, #19514 ) ;
#4910=CARTESIAN_POINT ( 'NONE',  ( -211.5106270998635409, 103.1299228374912360, 79.58252780074349175 ) ) ;
#4912=CIRCLE ( 'NONE', #13164, 10.00000000000000888 ) ;
#4923=DIRECTION ( 'NONE',  ( 1.000000000000000000, 5.889072920838430686E-16, -0.000000000000000000 ) ) ;
#4925=MECHANICAL_DESIGN_GEOMETRIC_PRESENTATION_REPRESENTATION('',(#8534),#18072);
#4928=ORIENTED_EDGE ( 'NONE', *, *, #12809, .T. ) ;
#4931=FACE_BOUND ( 'NONE', #2958, .T. ) ;
#4944=ORIENTED_EDGE ( 'NONE', *, *, #19600, .T. ) ;
#4956=DIRECTION ( 'NONE',  ( 1.000000000000000000, -0.000000000000000000, 0.000000000000000000 ) ) ;
#4966=AXIS2_PLACEMENT_3D ( 'NONE', #6740, #18764, #17 ) ;
#4967=VERTEX_POINT ( 'NONE', #129 ) ;
#4975=SURFACE_STYLE_USAGE ( .BOTH. , #1447 ) ;
#4977=VERTEX_POINT ( 'NONE', #15727 ) ;
#4981=STYLED_ITEM ( 'NONE', ( #4531 ), #11917 ) ;
#4985=CARTESIAN_POINT ( 'NONE',  ( 178.4893729001365728, 113.1299228374914918, 170.4174721992565082 ) ) ;
#5001=SURFACE_SIDE_STYLE ('',( #19211 ) ) ;
#5010=CARTESIAN_POINT ( 'NONE',  ( 78.48937290013661539, 80.91625508013694912, 250.0000000000000000 ) ) ;
#5021=ORIENTED_EDGE ( 'NONE', *, *, #14260, .F. ) ;
#5022=ADVANCED_FACE ( 'NONE', ( #31 ), #545, .F. ) ;
#5034=LINE ( 'NONE', #9455, #19244 ) ;
#5042=CARTESIAN_POINT ( 'NONE',  ( 0.000000000000000000, 0.000000000000000000, 0.000000000000000000 ) ) ;
#5045=CARTESIAN_POINT ( 'NONE',  ( 82.88953019741013861, 80.91625508013694912, 245.0000000000000000 ) ) ;
#5050=EDGE_LOOP ( 'NONE', ( #14108, #6176, #46, #19543 ) ) ;
#5065=LINE ( 'NONE', #3520, #4377 ) ;
#5066=DIRECTION ( 'NONE',  ( -0.000000000000000000, -0.000000000000000000, 1.000000000000000000 ) ) ;
#5073=AXIS2_PLACEMENT_3D ( 'NONE', #11789, #5694, #12092 ) ;
#5079=COLOUR_RGB ( '', 0.40784314, 0.44705882, 0.49803922) ;
#5082=CARTESIAN_POINT ( 'NONE',  ( -211.5106270998635409, 113.1299228374912502, 220.6387154965113382 ) ) ;
#5086=FILL_AREA_STYLE ('',( #8073 ) ) ;
#5101=AXIS2_PLACEMENT_3D ( 'NONE', #8128, #15555, #8015 ) ;
#5104=( GEOMETRIC_REPRESENTATION_CONTEXT ( 3 ) GLOBAL_UNCERTAINTY_ASSIGNED_CONTEXT ( ( #13366 ) ) GLOBAL_UNIT_ASSIGNED_CONTEXT ( ( #3122, #17741, #6940 ) ) REPRESENTATION_CONTEXT ( 'NONE', 'WORKASPACE' ) );
#5106=EDGE_CURVE ( 'NONE', #15013, #3589, #15105, .T. ) ;
#5126=PLANE ( 'NONE',  #18396 ) ;
#5132=FILL_AREA_STYLE ('',( #3476 ) ) ;
#5138=ORIENTED_EDGE ( 'NONE', *, *, #1293, .F. ) ;
#5152=DIRECTION ( 'NONE',  ( 0.000000000000000000, 0.000000000000000000, 1.000000000000000000 ) ) ;
#5159=FACE_OUTER_BOUND ( 'NONE', #1520, .T. ) ;
#5162=( LENGTH_UNIT ( ) NAMED_UNIT ( * ) SI_UNIT ( .MILLI., .METRE. ) );
#5206=ORIENTED_EDGE ( 'NONE', *, *, #20213, .T. ) ;
#5212=SURFACE_STYLE_USAGE ( .BOTH. , #10050 ) ;
#5214=EDGE_LOOP ( 'NONE', ( #19720, #13469, #2382, #5927 ) ) ;
#5222=DIRECTION ( 'NONE',  ( -1.000000000000000000, 0.000000000000000000, 0.000000000000000000 ) ) ;
#5223=SURFACE_STYLE_FILL_AREA ( #5425 ) ;
#5227=DIRECTION ( 'NONE',  ( 1.000000000000000000, 0.000000000000000000, -0.000000000000000000 ) ) ;
#5233=CARTESIAN_POINT ( 'NONE',  ( 78.48937290013660117, 123.1299228374914208, 220.6387154965113382 ) ) ;
#5234=EDGE_CURVE ( 'NONE', #19951, #5831, #2249, .T. ) ;
#5236=ORIENTED_EDGE ( 'NONE', *, *, #19210, .T. ) ;
#5247=DIRECTION ( 'NONE',  ( 0.000000000000000000, 1.000000000000000000, 0.000000000000000000 ) ) ;
#5256=AXIS2_PLACEMENT_3D ( 'NONE', #285, #17707, #14040 ) ;
#5257=MECHANICAL_DESIGN_GEOMETRIC_PRESENTATION_REPRESENTATION('',(#9189),#20032);
#5261=CARTESIAN_POINT ( 'NONE',  ( 78.48937290013660117, 145.9162550801369491, 0.000000000000000000 ) ) ;
#5266=FILL_AREA_STYLE ('',( #16408 ) ) ;
#5267=DIRECTION ( 'NONE',  ( 0.000000000000000000, 1.000000000000000000, 0.000000000000000000 ) ) ;
#5284=SURFACE_STYLE_FILL_AREA ( #11665 ) ;
#5288=ORIENTED_EDGE ( 'NONE', *, *, #5106, .F. ) ;
#5289=( NAMED_UNIT ( * ) SI_UNIT ( $, .STERADIAN. ) SOLID_ANGLE_UNIT ( ) );
#5291=LINE ( 'NONE', #10218, #17855 ) ;
#5295=DIRECTION ( 'NONE',  ( 1.000000000000000000, 5.889072920838430686E-16, -0.000000000000000000 ) ) ;
#5302=ORIENTED_EDGE ( 'NONE', *, *, #6342, .F. ) ;
#5308=ORIENTED_EDGE ( 'NONE', *, *, #7423, .T. ) ;
#5309=DIRECTION ( 'NONE',  ( 0.000000000000000000, 0.000000000000000000, 1.000000000000000000 ) ) ;
#5312=VERTEX_POINT ( 'NONE', #2017 ) ;
#5313=MECHANICAL_DESIGN_GEOMETRIC_PRESENTATION_REPRESENTATION('',(#15839),#3978);
#5316=SURFACE_STYLE_FILL_AREA ( #8709 ) ;
#5318=DIRECTION ( 'NONE',  ( 1.000000000000000000, 2.135044278125300850E-16, -0.000000000000000000 ) ) ;
#5320=SURFACE_SIDE_STYLE ('',( #19411 ) ) ;
#5329=EDGE_CURVE ( 'NONE', #1058, #2483, #4912, .T. ) ;
#5345=ORIENTED_EDGE ( 'NONE', *, *, #14145, .F. ) ;
#5348=EDGE_CURVE ( 'NONE', #14026, #20243, #14450, .T. ) ;
#5353=EDGE_CURVE ( 'NONE', #1341, #3236, #6593, .T. ) ;
#5371=ADVANCED_FACE ( 'NONE', ( #16480 ), #883, .T. ) ;
#5392=DIRECTION ( 'NONE',  ( -1.000000000000000000, 0.000000000000000000, 0.000000000000000000 ) ) ;
#5398=SURFACE_SIDE_STYLE ('',( #11374 ) ) ;
#5402=CARTESIAN_POINT ( 'NONE',  ( 153.4893729001366864, 113.1299228374914634, 29.36128450348865471 ) ) ;
#5412=STYLED_ITEM ( 'NONE', ( #540 ), #14853 ) ;
#5415=( GEOMETRIC_REPRESENTATION_CONTEXT ( 3 ) GLOBAL_UNCERTAINTY_ASSIGNED_CONTEXT ( ( #17941 ) ) GLOBAL_UNIT_ASSIGNED_CONTEXT ( ( #19896, #10632, #18260 ) ) REPRESENTATION_CONTEXT ( 'NONE', 'WORKASPACE' ) );
#5417=SURFACE_STYLE_USAGE ( .BOTH. , #10056 ) ;
#5425=FILL_AREA_STYLE ('',( #19414 ) ) ;
#5436=VERTEX_POINT ( 'NONE', #11622 ) ;
#5437=ORIENTED_EDGE ( 'NONE', *, *, #12060, .F. ) ;
#5451=DIRECTION ( 'NONE',  ( 1.000000000000000000, 0.000000000000000000, 0.000000000000000000 ) ) ;
#5455=( LENGTH_UNIT ( ) NAMED_UNIT ( * ) SI_UNIT ( .MILLI., .METRE. ) );
#5465=CARTESIAN_POINT ( 'NONE',  ( 53.48937290013659407, 145.9162550801369491, 0.000000000000000000 ) ) ;
#5478=STYLED_ITEM ( 'NONE', ( #20157 ), #9624 ) ;
#5486=( LENGTH_UNIT ( ) NAMED_UNIT ( * ) SI_UNIT ( .MILLI., .METRE. ) );
#5489=( NAMED_UNIT ( * ) PLANE_ANGLE_UNIT ( ) SI_UNIT ( $, .RADIAN. ) );
#5491=CARTESIAN_POINT ( 'NONE',  ( -211.5106270998635409, 103.1299228374912360, 220.6387154965113382 ) ) ;
#5495=FACE_OUTER_BOUND ( 'NONE', #15548, .T. ) ;
#5498=ADVANCED_FACE ( 'NONE', ( #12443 ), #17074, .F. ) ;
#5502=DIRECTION ( 'NONE',  ( 1.000000000000000000, 0.000000000000000000, 0.000000000000000000 ) ) ;
#5510=ORIENTED_EDGE ( 'NONE', *, *, #1418, .F. ) ;
#5513=UNCERTAINTY_MEASURE_WITH_UNIT (LENGTH_MEASURE( 1.000000000000000082E-05 ), #3497, 'distance_accuracy_value', 'NONE');
#5518=ORIENTED_EDGE ( 'NONE', *, *, #7759, .F. ) ;
#5521=DIRECTION ( 'NONE',  ( 1.000000000000000000, 9.815121534730717399E-17, -0.000000000000000000 ) ) ;
#5523=ADVANCED_FACE ( 'NONE', ( #13875 ), #6055, .F. ) ;
#5524=VERTEX_POINT ( 'NONE', #18156 ) ;
#5528=EDGE_LOOP ( 'NONE', ( #9193, #11605 ) ) ;
#5532=ORIENTED_EDGE ( 'NONE', *, *, #314, .T. ) ;
#5533=CARTESIAN_POINT ( 'NONE',  ( 88.88953019741013861, 80.91625508013694912, 245.0000000000000000 ) ) ;
#5536=LINE ( 'NONE', #19339, #13890 ) ;
#5543=PRESENTATION_STYLE_ASSIGNMENT (( #7300 ) ) ;
#5547=ORIENTED_EDGE ( 'NONE', *, *, #3219, .F. ) ;
#5555=COLOUR_RGB ( '', 0.09019608, 0.27058824, 0.51372549) ;
#5568=( GEOMETRIC_REPRESENTATION_CONTEXT ( 3 ) GLOBAL_UNCERTAINTY_ASSIGNED_CONTEXT ( ( #16151 ) ) GLOBAL_UNIT_ASSIGNED_CONTEXT ( ( #8626, #14925, #2136 ) ) REPRESENTATION_CONTEXT ( 'NONE', 'WORKASPACE' ) );
#5569=COLOUR_RGB ( '', 0.72549020, 0.75294118, 0.79215686) ;
#5602=( NAMED_UNIT ( * ) PLANE_ANGLE_UNIT ( ) SI_UNIT ( $, .RADIAN. ) );
#5603=CARTESIAN_POINT ( 'NONE',  ( 53.48937290013659407, 145.9162550801369491, 0.000000000000000000 ) ) ;
#5611=VECTOR ( 'NONE', #2179, 1000.000000000000000 ) ;
#5612=STYLED_ITEM ( 'NONE', ( #5680 ), #6193 ) ;
#5614=VERTEX_POINT ( 'NONE', #11701 ) ;
#5615=( NAMED_UNIT ( * ) PLANE_ANGLE_UNIT ( ) SI_UNIT ( $, .RADIAN. ) );
#5617=SURFACE_STYLE_USAGE ( .BOTH. , #20120 ) ;
#5635=DIRECTION ( 'NONE',  ( 1.000000000000000000, 0.000000000000000000, 0.000000000000000000 ) ) ;
#5643=VECTOR ( 'NONE', #12899, 1000.000000000000000 ) ;
#5651=ORIENTED_EDGE ( 'NONE', *, *, #18438, .T. ) ;
#5652=CARTESIAN_POINT ( 'NONE',  ( -211.5106270998635409, 123.1299228374912644, 29.36128450348865471 ) ) ;
#5658=LINE ( 'NONE', #10597, #7031 ) ;
#5666=DIRECTION ( 'NONE',  ( 0.000000000000000000, -1.000000000000000000, 0.000000000000000000 ) ) ;
#5667=COLOUR_RGB ( '', 0.09019608, 0.27058824, 0.51372549) ;
#5671=COLOUR_RGB ( '', 0.66274510, 0.83137255, 0.94901961) ;
#5676=LINE ( 'NONE', #4338, #3675 ) ;
#5680=PRESENTATION_STYLE_ASSIGNMENT (( #2579 ) ) ;
#5685=DIRECTION ( 'NONE',  ( 0.000000000000000000, 0.000000000000000000, 1.000000000000000000 ) ) ;
#5694=DIRECTION ( 'NONE',  ( 0.000000000000000000, -1.000000000000000000, 0.000000000000000000 ) ) ;
#5706=( NAMED_UNIT ( * ) SI_UNIT ( $, .STERADIAN. ) SOLID_ANGLE_UNIT ( ) );
#5709=AXIS2_PLACEMENT_3D ( 'NONE', #7479, #12198, #11910 ) ;
#5713=CARTESIAN_POINT ( 'NONE',  ( 82.88953019741013861, 167.9162550801369491, 245.0000000000000000 ) ) ;
#5714=PRESENTATION_STYLE_ASSIGNMENT (( #5617 ) ) ;
#5718=EDGE_CURVE ( 'NONE', #4612, #10163, #17767, .T. ) ;
#5722=( GEOMETRIC_REPRESENTATION_CONTEXT ( 3 ) GLOBAL_UNCERTAINTY_ASSIGNED_CONTEXT ( ( #16700 ) ) GLOBAL_UNIT_ASSIGNED_CONTEXT ( ( #11287, #14082, #10888 ) ) REPRESENTATION_CONTEXT ( 'NONE', 'WORKASPACE' ) );
#5733=EDGE_LOOP ( 'NONE', ( #3222, #13031 ) ) ;
#5734=LINE ( 'NONE', #3348, #7431 ) ;
#5737=CARTESIAN_POINT ( 'NONE',  ( 78.48937290013660117, 113.1299228374914208, 79.58252780074349175 ) ) ;
#5748=AXIS2_PLACEMENT_3D ( 'NONE', #109, #7847, #14127 ) ;
#5750=DIRECTION ( 'NONE',  ( 0.000000000000000000, -1.000000000000000000, 0.000000000000000000 ) ) ;
#5753=PLANE ( 'NONE',  #11596 ) ;
#5766=ORIENTED_EDGE ( 'NONE', *, *, #10125, .T. ) ;
#5773=CIRCLE ( 'NONE', #6434, 10.00000000000000888 ) ;
#5786=AXIS2_PLACEMENT_3D ( 'NONE', #8564, #17847, #19586 ) ;
#5797=( NAMED_UNIT ( * ) PLANE_ANGLE_UNIT ( ) SI_UNIT ( $, .RADIAN. ) );
#5811=ORIENTED_EDGE ( 'NONE', *, *, #12073, .T. ) ;
#5817=FACE_BOUND ( 'NONE', #9736, .T. ) ;
#5819=AXIS2_PLACEMENT_3D ( 'NONE', #15666, #12233, #4309 ) ;
#5831=VERTEX_POINT ( 'NONE', #18057 ) ;
#5857=ORIENTED_EDGE ( 'NONE', *, *, #5329, .T. ) ;
#5859=AXIS2_PLACEMENT_3D ( 'NONE', #6995, #14920, #14810 ) ;
#5873=AXIS2_PLACEMENT_3D ( 'NONE', #12330, #1362, #18708 ) ;
#5874=( NAMED_UNIT ( * ) SI_UNIT ( $, .STERADIAN. ) SOLID_ANGLE_UNIT ( ) );
#5876=DIRECTION ( 'NONE',  ( 1.000000000000000000, 5.889072920838430686E-16, -0.000000000000000000 ) ) ;
#5877=FACE_OUTER_BOUND ( 'NONE', #5214, .T. ) ;
#5883=ORIENTED_EDGE ( 'NONE', *, *, #10136, .T. ) ;
#5888=DIRECTION ( 'NONE',  ( 0.000000000000000000, -1.000000000000000000, 0.000000000000000000 ) ) ;
#5899=VERTEX_POINT ( 'NONE', #4059 ) ;
#5901=SURFACE_STYLE_FILL_AREA ( #17115 ) ;
#5907=VERTEX_POINT ( 'NONE', #7356 ) ;
#5923=MECHANICAL_DESIGN_GEOMETRIC_PRESENTATION_REPRESENTATION('',(#14467),#16145);
#5927=ORIENTED_EDGE ( 'NONE', *, *, #443, .T. ) ;
#5958=DIRECTION ( 'NONE',  ( -0.000000000000000000, -1.000000000000000000, -0.000000000000000000 ) ) ;
#5966=DIRECTION ( 'NONE',  ( 0.000000000000000000, 1.000000000000000000, 0.000000000000000000 ) ) ;
#5967=FACE_OUTER_BOUND ( 'NONE', #12240, .T. ) ;
#5969=ADVANCED_FACE ( 'NONE', ( #1224, #5817, #2395, #8700, #12098 ), #853, .F. ) ;
#5977=EDGE_CURVE ( 'NONE', #6311, #9122, #15824, .T. ) ;
#5980=ORIENTED_EDGE ( 'NONE', *, *, #7129, .T. ) ;
#5984=CYLINDRICAL_SURFACE ( 'NONE', #1080, 10.00000000000000888 ) ;
#5986=CARTESIAN_POINT ( 'NONE',  ( -211.5106270998635409, 113.1299228374912502, 220.6387154965113382 ) ) ;
#5995=DIRECTION ( 'NONE',  ( 0.000000000000000000, 1.000000000000000000, 0.000000000000000000 ) ) ;
#6002=AXIS2_PLACEMENT_3D ( 'NONE', #6587, #4723, #17602 ) ;
#6012=( LENGTH_UNIT ( ) NAMED_UNIT ( * ) SI_UNIT ( .MILLI., .METRE. ) );
#6015=EDGE_CURVE ( 'NONE', #15858, #21, #3123, .T. ) ;
#6025=( NAMED_UNIT ( * ) PLANE_ANGLE_UNIT ( ) SI_UNIT ( $, .RADIAN. ) );
#6031=EDGE_LOOP ( 'NONE', ( #17160, #1612, #15447, #4564 ) ) ;
#6033=AXIS2_PLACEMENT_3D ( 'NONE', #234, #814, #8767 ) ;
#6044=DIRECTION ( 'NONE',  ( 1.000000000000000000, 5.889072920838430686E-16, -0.000000000000000000 ) ) ;
#6048=MECHANICAL_DESIGN_GEOMETRIC_PRESENTATION_REPRESENTATION('',(#11652),#10324);
#6052=DIRECTION ( 'NONE',  ( -1.000000000000000000, -1.595148023886719315E-16, 0.000000000000000000 ) ) ;
#6055=PLANE ( 'NONE',  #19707 ) ;
#6062=ORIENTED_EDGE ( 'NONE', *, *, #5234, .T. ) ;
#6063=( GEOMETRIC_REPRESENTATION_CONTEXT ( 3 ) GLOBAL_UNCERTAINTY_ASSIGNED_CONTEXT ( ( #15086 ) ) GLOBAL_UNIT_ASSIGNED_CONTEXT ( ( #10448, #4268, #5706 ) ) REPRESENTATION_CONTEXT ( 'NONE', 'WORKASPACE' ) );
#6078=CARTESIAN_POINT ( 'NONE',  ( 98.48937290013660117, 167.9162550801369491, -97.94896630388704750 ) ) ;
#6088=STYLED_ITEM ( 'NONE', ( #9839 ), #10258 ) ;
#6091=COLOUR_RGB ( '', 0.31764706, 0.68627451, 0.89019608) ;
#6099=VERTEX_POINT ( 'NONE', #2169 ) ;
#6100=DIRECTION ( 'NONE',  ( -2.135044278125300850E-16, 1.000000000000000000, 0.000000000000000000 ) ) ;
#6112=AXIS2_PLACEMENT_3D ( 'NONE', #16500, #7126, #16611 ) ;
#6121=ADVANCED_FACE ( 'NONE', ( #8474 ), #14752, .F. ) ;
#6125=DIRECTION ( 'NONE',  ( 1.000000000000000000, -0.000000000000000000, 0.000000000000000000 ) ) ;
#6139=PRESENTATION_STYLE_ASSIGNMENT (( #4481 ) ) ;
#6147=VERTEX_POINT ( 'NONE', #10020 ) ;
#6168=FILL_AREA_STYLE ('',( #20040 ) ) ;
#6176=ORIENTED_EDGE ( 'NONE', *, *, #1627, .F. ) ;
#6179=EDGE_LOOP ( 'NONE', ( #18627, #13539, #19490, #10927 ) ) ;
#6193=ADVANCED_FACE ( 'NONE', ( #2059 ), #19378, .T. ) ;
#6194=VERTEX_POINT ( 'NONE', #8559 ) ;
#6197=CARTESIAN_POINT ( 'NONE',  ( 143.0892156028631348, 167.9162550801369491, 245.0000000000000000 ) ) ;
#6202=PRESENTATION_STYLE_ASSIGNMENT (( #2984 ) ) ;
#6206=CARTESIAN_POINT ( 'NONE',  ( 133.4893729001365443, 113.1299228374914634, 29.36128450348865471 ) ) ;
#6214=ADVANCED_FACE ( 'NONE', ( #8969 ), #13433, .F. ) ;
#6224=AXIS2_PLACEMENT_3D ( 'NONE', #2071, #2383, #8393 ) ;
#6232=FACE_OUTER_BOUND ( 'NONE', #3446, .T. ) ;
#6237=ORIENTED_EDGE ( 'NONE', *, *, #13819, .F. ) ;
#6238=AXIS2_PLACEMENT_3D ( 'NONE', #5082, #17742, #6743 ) ;
#6241=AXIS2_PLACEMENT_3D ( 'NONE', #15096, #9197, #19911 ) ;
#6263=CARTESIAN_POINT ( 'NONE',  ( 98.48937290013662960, 1.571051285554951424E-14, 0.000000000000000000 ) ) ;
#6266=DIRECTION ( 'NONE',  ( 1.000000000000000000, 0.000000000000000000, 0.000000000000000000 ) ) ;
#6276=CARTESIAN_POINT ( 'NONE',  ( -211.5106270998635409, 113.1299228374912502, 29.36128450348865471 ) ) ;
#6282=ADVANCED_FACE ( 'NONE', ( #2785 ), #18544, .F. ) ;
#6287=CIRCLE ( 'NONE', #17784, 10.00000000000000888 ) ;
#6293=ORIENTED_EDGE ( 'NONE', *, *, #16438, .F. ) ;
#6296=ORIENTED_EDGE ( 'NONE', *, *, #4236, .T. ) ;
#6297=EDGE_LOOP ( 'NONE', ( #18126, #2622, #14627, #16997 ) ) ;
#6300=COLOUR_RGB ( '', 0.09019608, 0.27058824, 0.51372549) ;
#6304=CARTESIAN_POINT ( 'NONE',  ( 78.48937290013661539, 80.91625508013694912, 0.000000000000000000 ) ) ;
#6308=CARTESIAN_POINT ( 'NONE',  ( 133.4893729001365443, 103.1299228374914492, 170.4174721992565082 ) ) ;
#6311=VERTEX_POINT ( 'NONE', #3713 ) ;
#6313=FACE_OUTER_BOUND ( 'NONE', #4022, .T. ) ;
#6317=CYLINDRICAL_SURFACE ( 'NONE', #2983, 10.00000000000000888 ) ;
#6334=ORIENTED_EDGE ( 'NONE', *, *, #7017, .F. ) ;
#6336=CARTESIAN_POINT ( 'NONE',  ( 98.48937290013662960, 123.1299228374914350, 170.4174721992565082 ) ) ;
#6342=EDGE_CURVE ( 'NONE', #16841, #19266, #206, .T. ) ;
#6352=DIRECTION ( 'NONE',  ( 0.000000000000000000, -0.000000000000000000, -1.000000000000000000 ) ) ;
#6362=LINE ( 'NONE', #17165, #10378 ) ;
#6364=VECTOR ( 'NONE', #1309, 1000.000000000000000 ) ;
#6369=CIRCLE ( 'NONE', #11626, 10.00000000000000888 ) ;
#6382=DIRECTION ( 'NONE',  ( -1.000000000000000000, 0.000000000000000000, 0.000000000000000000 ) ) ;
#6416=CARTESIAN_POINT ( 'NONE',  ( 143.0892156028631348, 80.91625508013694912, 245.0000000000000000 ) ) ;
#6427=STYLED_ITEM ( 'NONE', ( #11307 ), #10768 ) ;
#6428=SURFACE_SIDE_STYLE ('',( #19066 ) ) ;
#6434=AXIS2_PLACEMENT_3D ( 'NONE', #255, #11395, #9329 ) ;
#6437=CARTESIAN_POINT ( 'NONE',  ( 78.48937290013660117, 113.1299228374914208, 170.4174721992565082 ) ) ;
#6443=AXIS2_PLACEMENT_3D ( 'NONE', #17058, #4492, #1053 ) ;
#6461=VERTEX_POINT ( 'NONE', #11642 ) ;
#6482=PLANE ( 'NONE',  #18264 ) ;
#6494=EDGE_CURVE ( 'NONE', #3886, #8633, #8222, .T. ) ;
#6515=FILL_AREA_STYLE ('',( #17116 ) ) ;
#6537=ORIENTED_EDGE ( 'NONE', *, *, #15864, .F. ) ;
#6545=VERTEX_POINT ( 'NONE', #18636 ) ;
#6550=ORIENTED_EDGE ( 'NONE', *, *, #3452, .F. ) ;
#6553=CARTESIAN_POINT ( 'NONE',  ( 78.48937290013660117, 113.1299228374914208, 29.36128450348865471 ) ) ;
#6555=FACE_OUTER_BOUND ( 'NONE', #11003, .T. ) ;
#6557=CARTESIAN_POINT ( 'NONE',  ( 153.4893729001366580, 80.91625508013694912, 0.000000000000000000 ) ) ;
#6558=CARTESIAN_POINT ( 'NONE',  ( 178.4893729001365443, 145.9162550801369491, 250.0000000000000000 ) ) ;
#6563=( LENGTH_UNIT ( ) NAMED_UNIT ( * ) SI_UNIT ( .MILLI., .METRE. ) );
#6567=VECTOR ( 'NONE', #3615, 1000.000000000000000 ) ;
#6568=AXIS2_PLACEMENT_3D ( 'NONE', #8142, #12992, #12883 ) ;
#6574=ORIENTED_EDGE ( 'NONE', *, *, #15524, .F. ) ;
#6582=FACE_OUTER_BOUND ( 'NONE', #669, .T. ) ;
#6584=COLOUR_RGB ( '', 0.66274510, 0.83137255, 0.94901961) ;
#6587=CARTESIAN_POINT ( 'NONE',  ( 98.48937290013662960, 113.1299228374914350, 79.58252780074349175 ) ) ;
#6593=LINE ( 'NONE', #5045, #7545 ) ;
#6610=CIRCLE ( 'NONE', #15507, 10.00000000000000888 ) ;
#6623=AXIS2_PLACEMENT_3D ( 'NONE', #15817, #4791, #12508 ) ;
#6630=ORIENTED_EDGE ( 'NONE', *, *, #7619, .F. ) ;
#6654=EDGE_CURVE ( 'NONE', #2115, #1665, #14500, .T. ) ;
#6655=VERTEX_POINT ( 'NONE', #15987 ) ;
#6661=CARTESIAN_POINT ( 'NONE',  ( -211.5106270998635409, 103.1299228374912360, 29.36128450348865471 ) ) ;
#6681=EDGE_CURVE ( 'NONE', #11219, #17540, #13095, .T. ) ;
#6713=CIRCLE ( 'NONE', #18858, 10.00000000000000888 ) ;
#6724=LINE ( 'NONE', #15896, #15252 ) ;
#6726=( GEOMETRIC_REPRESENTATION_CONTEXT ( 3 ) GLOBAL_UNCERTAINTY_ASSIGNED_CONTEXT ( ( #15296 ) ) GLOBAL_UNIT_ASSIGNED_CONTEXT ( ( #15887, #18952, #9477 ) ) REPRESENTATION_CONTEXT ( 'NONE', 'WORKASPACE' ) );
#6728=CARTESIAN_POINT ( 'NONE',  ( 78.48937290013660117, 113.1299228374914208, 79.58252780074349175 ) ) ;
#6738=MECHANICAL_DESIGN_GEOMETRIC_PRESENTATION_REPRESENTATION('',(#11651),#6063);
#6740=CARTESIAN_POINT ( 'NONE',  ( -211.5106270998635409, 113.1299228374912502, 29.36128450348865471 ) ) ;
#6743=DIRECTION ( 'NONE',  ( 0.000000000000000000, 1.000000000000000000, 0.000000000000000000 ) ) ;
#6746=FACE_OUTER_BOUND ( 'NONE', #18883, .T. ) ;
#6754=CARTESIAN_POINT ( 'NONE',  ( 178.4893729001366012, 34.32473510485366575, 250.0000000000000000 ) ) ;
#6755=LINE ( 'NONE', #16429, #5611 ) ;
#6759=FILL_AREA_STYLE ('',( #9827 ) ) ;
#6765=EDGE_CURVE ( 'NONE', #13737, #17589, #16473, .T. ) ;
#6767=ORIENTED_EDGE ( 'NONE', *, *, #8849, .T. ) ;
#6773=FACE_OUTER_BOUND ( 'NONE', #13878, .T. ) ;
#6785=SURFACE_STYLE_FILL_AREA ( #5132 ) ;
#6808=CARTESIAN_POINT ( 'NONE',  ( 53.48937290013658696, 103.1299228374913923, 29.36128450348865471 ) ) ;
#6812=DIRECTION ( 'NONE',  ( 1.000000000000000000, 5.889072920838430686E-16, -0.000000000000000000 ) ) ;
#6815=FILL_AREA_STYLE ('',( #16095 ) ) ;
#6816=ORIENTED_EDGE ( 'NONE', *, *, #370, .F. ) ;
#6828=FACE_BOUND ( 'NONE', #2832, .T. ) ;
#6848=SURFACE_STYLE_FILL_AREA ( #8379 ) ;
#6852=CARTESIAN_POINT ( 'NONE',  ( 88.88953019741013861, 80.91625508013694912, 245.0000000000000000 ) ) ;
#6856=CARTESIAN_POINT ( 'NONE',  ( 53.48937290013659407, 145.9162550801369491, 0.000000000000000000 ) ) ;
#6857=VECTOR ( 'NONE', #8565, 1000.000000000000000 ) ;
#6865=UNCERTAINTY_MEASURE_WITH_UNIT (LENGTH_MEASURE( 1.000000000000000082E-05 ), #2202, 'distance_accuracy_value', 'NONE');
#6875=ORIENTED_EDGE ( 'NONE', *, *, #3627, .T. ) ;
#6877=DIRECTION ( 'NONE',  ( 0.000000000000000000, 1.000000000000000000, 0.000000000000000000 ) ) ;
#6887=EDGE_CURVE ( 'NONE', #15013, #10819, #18388, .T. ) ;
#6893=CARTESIAN_POINT ( 'NONE',  ( 53.48937290013659407, 0.000000000000000000, 0.000000000000000000 ) ) ;
#6911=AXIS2_PLACEMENT_3D ( 'NONE', #3504, #8342, #18006 ) ;
#6913=COLOUR_RGB ( '', 0.31764706, 0.68627451, 0.89019608) ;
#6914=ORIENTED_EDGE ( 'NONE', *, *, #2184, .F. ) ;
#6915=ORIENTED_EDGE ( 'NONE', *, *, #15928, .F. ) ;
#6917=DIRECTION ( 'NONE',  ( 1.000000000000000000, 5.889072920838430686E-16, -0.000000000000000000 ) ) ;
#6937=ADVANCED_FACE ( 'NONE', ( #7583 ), #8921, .F. ) ;
#6940=( NAMED_UNIT ( * ) SI_UNIT ( $, .STERADIAN. ) SOLID_ANGLE_UNIT ( ) );
#6941=FILL_AREA_STYLE_COLOUR ( '', #13830 ) ;
#6946=PLANE ( 'NONE',  #7662 ) ;
#6952=FACE_OUTER_BOUND ( 'NONE', #7953, .T. ) ;
#6956=EDGE_LOOP ( 'NONE', ( #4829, #1238, #4587, #16771 ) ) ;
#6961=VERTEX_POINT ( 'NONE', #15535 ) ;
#6963=DIRECTION ( 'NONE',  ( 0.000000000000000000, 1.000000000000000000, -0.000000000000000000 ) ) ;
#6965=DIRECTION ( 'NONE',  ( 1.000000000000000000, 5.889072920838430686E-16, 0.000000000000000000 ) ) ;
#6993=ADVANCED_FACE ( 'NONE', ( #6555 ), #4901, .F. ) ;
#6995=CARTESIAN_POINT ( 'NONE',  ( 78.48937290013660117, 113.1299228374914208, 220.6387154965113382 ) ) ;
#7009=CIRCLE ( 'NONE', #708, 10.00000000000000888 ) ;
#7017=EDGE_CURVE ( 'NONE', #7147, #10363, #12844, .T. ) ;
#7027=AXIS2_PLACEMENT_3D ( 'NONE', #16446, #18060, #2290 ) ;
#7031=VECTOR ( 'NONE', #7217, 1000.000000000000000 ) ;
#7035=UNCERTAINTY_MEASURE_WITH_UNIT (LENGTH_MEASURE( 1.000000000000000082E-05 ), #18526, 'distance_accuracy_value', 'NONE');
#7040=( NAMED_UNIT ( * ) PLANE_ANGLE_UNIT ( ) SI_UNIT ( $, .RADIAN. ) );
#7043=PRESENTATION_STYLE_ASSIGNMENT (( #2488 ) ) ;
#7045=SURFACE_STYLE_USAGE ( .BOTH. , #17340 ) ;
#7048=AXIS2_PLACEMENT_3D ( 'NONE', #19769, #3927, #11270 ) ;
#7055=COLOUR_RGB ( '', 0.31764706, 0.68627451, 0.89019608) ;
#7059=ORIENTED_EDGE ( 'NONE', *, *, #16790, .F. ) ;
#7063=( GEOMETRIC_REPRESENTATION_CONTEXT ( 3 ) GLOBAL_UNCERTAINTY_ASSIGNED_CONTEXT ( ( #10519 ) ) GLOBAL_UNIT_ASSIGNED_CONTEXT ( ( #8571, #12935, #19197 ) ) REPRESENTATION_CONTEXT ( 'NONE', 'WORKASPACE' ) );
#7069=( LENGTH_UNIT ( ) NAMED_UNIT ( * ) SI_UNIT ( .MILLI., .METRE. ) );
#7070=MECHANICAL_DESIGN_GEOMETRIC_PRESENTATION_REPRESENTATION('',(#1093),#5415);
#7080=( NAMED_UNIT ( * ) SI_UNIT ( $, .STERADIAN. ) SOLID_ANGLE_UNIT ( ) );
#7081=CIRCLE ( 'NONE', #13662, 10.00000000000000888 ) ;
#7083=CIRCLE ( 'NONE', #18893, 10.00000000000000888 ) ;
#7088=AXIS2_PLACEMENT_3D ( 'NONE', #5737, #2629, #2733 ) ;
#7090=ORIENTED_EDGE ( 'NONE', *, *, #14342, .F. ) ;
#7107=SURFACE_SIDE_STYLE ('',( #788 ) ) ;
#7110=CARTESIAN_POINT ( 'NONE',  ( -211.5106270998635409, 113.1299228374912502, 79.58252780074349175 ) ) ;
#7116=EDGE_CURVE ( 'NONE', #995, #4612, #9544, .T. ) ;
#7126=DIRECTION ( 'NONE',  ( 1.000000000000000000, 0.000000000000000000, 0.000000000000000000 ) ) ;
#7127=SURFACE_STYLE_FILL_AREA ( #15249 ) ;
#7129=EDGE_CURVE ( 'NONE', #530, #10363, #11638, .T. ) ;
#7131=CARTESIAN_POINT ( 'NONE',  ( 0.000000000000000000, 145.9162550801369491, -97.94896630388704750 ) ) ;
#7140=VERTEX_POINT ( 'NONE', #2553 ) ;
#7145=( LENGTH_UNIT ( ) NAMED_UNIT ( * ) SI_UNIT ( .MILLI., .METRE. ) );
#7147=VERTEX_POINT ( 'NONE', #14825 ) ;
#7163=ORIENTED_EDGE ( 'NONE', *, *, #15524, .T. ) ;
#7174=UNCERTAINTY_MEASURE_WITH_UNIT (LENGTH_MEASURE( 1.000000000000000082E-05 ), #12636, 'distance_accuracy_value', 'NONE');
#7175=CARTESIAN_POINT ( 'NONE',  ( -211.5106270998635409, 113.1299228374912502, 220.6387154965113382 ) ) ;
#7179=ORIENTED_EDGE ( 'NONE', *, *, #8122, .T. ) ;
#7203=DIRECTION ( 'NONE',  ( 0.000000000000000000, 1.000000000000000000, -0.000000000000000000 ) ) ;
#7208=EDGE_CURVE ( 'NONE', #14262, #14090, #7420, .T. ) ;
#7217=DIRECTION ( 'NONE',  ( 1.000000000000000000, 5.889072920838430686E-16, -0.000000000000000000 ) ) ;
#7220=LINE ( 'NONE', #12929, #20163 ) ;
#7221=SURFACE_STYLE_USAGE ( .BOTH. , #4423 ) ;
#7227=EDGE_CURVE ( 'NONE', #7485, #15108, #6287, .T. ) ;
#7228=ORIENTED_EDGE ( 'NONE', *, *, #11522, .F. ) ;
#7235=SURFACE_STYLE_FILL_AREA ( #3931 ) ;
#7237=( LENGTH_UNIT ( ) NAMED_UNIT ( * ) SI_UNIT ( .MILLI., .METRE. ) );
#7251=ADVANCED_FACE ( 'NONE', ( #1086 ), #15907, .F. ) ;
#7265=CIRCLE ( 'NONE', #15820, 10.00000000000000888 ) ;
#7273=SURFACE_SIDE_STYLE ('',( #2714 ) ) ;
#7277=ORIENTED_EDGE ( 'NONE', *, *, #6015, .T. ) ;
#7280=ORIENTED_EDGE ( 'NONE', *, *, #14451, .T. ) ;
#7285=DIRECTION ( 'NONE',  ( 1.000000000000000000, 5.889072920838430686E-16, -0.000000000000000000 ) ) ;
#7300=SURFACE_STYLE_USAGE ( .BOTH. , #7107 ) ;
#7303=ORIENTED_EDGE ( 'NONE', *, *, #3084, .F. ) ;
#7315=FACE_BOUND ( 'NONE', #8801, .T. ) ;
#7316=CARTESIAN_POINT ( 'NONE',  ( 53.48937290013659407, 145.9162550801369491, 250.0000000000000000 ) ) ;
#7319=EDGE_CURVE ( 'NONE', #21, #5614, #3217, .T. ) ;
#7324=VECTOR ( 'NONE', #5635, 1000.000000000000000 ) ;
#7328=CARTESIAN_POINT ( 'NONE',  ( 78.48937290013660117, 145.9162550801369491, 250.0000000000000000 ) ) ;
#7330=CARTESIAN_POINT ( 'NONE',  ( 78.48937290013660117, 113.1299228374914208, 220.6387154965113382 ) ) ;
#7335=LINE ( 'NONE', #18445, #11021 ) ;
#7341=DIRECTION ( 'NONE',  ( 1.000000000000000000, 5.889072920838430686E-16, -0.000000000000000000 ) ) ;
#7355=CARTESIAN_POINT ( 'NONE',  ( 0.000000000000000000, 0.000000000000000000, 250.0000000000000000 ) ) ;
#7356=CARTESIAN_POINT ( 'NONE',  ( 153.4893729001366864, 103.1299228374914492, 29.36128450348865471 ) ) ;
#7359=CARTESIAN_POINT ( 'NONE',  ( 0.000000000000000000, 0.000000000000000000, 0.000000000000000000 ) ) ;
#7362=ADVANCED_FACE ( 'NONE', ( #116 ), #17425, .F. ) ;
#7366=DIRECTION ( 'NONE',  ( 0.000000000000000000, 0.000000000000000000, -1.000000000000000000 ) ) ;
#7367=ADVANCED_FACE ( 'NONE', ( #18862 ), #6317, .F. ) ;
#7378=ORIENTED_EDGE ( 'NONE', *, *, #16628, .F. ) ;
#7416=VECTOR ( 'NONE', #3543, 1000.000000000000000 ) ;
#7420=LINE ( 'NONE', #17362, #14490 ) ;
#7423=EDGE_CURVE ( 'NONE', #6147, #825, #17133, .T. ) ;
#7431=VECTOR ( 'NONE', #7285, 1000.000000000000000 ) ;
#7453=CARTESIAN_POINT ( 'NONE',  ( 98.48937290013662960, 1.571051285554951424E-14, 250.0000000000000000 ) ) ;
#7466=UNCERTAINTY_MEASURE_WITH_UNIT (LENGTH_MEASURE( 1.000000000000000082E-05 ), #12633, 'distance_accuracy_value', 'NONE');
#7467=ORIENTED_EDGE ( 'NONE', *, *, #2971, .F. ) ;
#7479=CARTESIAN_POINT ( 'NONE',  ( 53.48937290013659407, 145.9162550801369491, 250.0000000000000000 ) ) ;
#7484=SURFACE_SIDE_STYLE ('',( #11811 ) ) ;
#7485=VERTEX_POINT ( 'NONE', #11874 ) ;
#7499=DIRECTION ( 'NONE',  ( 0.000000000000000000, -1.000000000000000000, 0.000000000000000000 ) ) ;
#7501=ADVANCED_FACE ( 'NONE', ( #14967 ), #13330, .F. ) ;
#7503=LINE ( 'NONE', #15343, #13491 ) ;
#7506=EDGE_CURVE ( 'NONE', #1681, #4967, #18344, .T. ) ;
#7512=( NAMED_UNIT ( * ) PLANE_ANGLE_UNIT ( ) SI_UNIT ( $, .RADIAN. ) );
#7516=ORIENTED_EDGE ( 'NONE', *, *, #15828, .T. ) ;
#7532=EDGE_LOOP ( 'NONE', ( #17519, #17834, #8800, #19546 ) ) ;
#7544=CARTESIAN_POINT ( 'NONE',  ( 78.48937290013660117, 113.1299228374914208, 79.58252780074349175 ) ) ;
#7545=VECTOR ( 'NONE', #19263, 1000.000000000000000 ) ;
#7559=SURFACE_SIDE_STYLE ('',( #1228 ) ) ;
#7565=DIRECTION ( 'NONE',  ( 0.000000000000000000, -0.000000000000000000, -1.000000000000000000 ) ) ;
#7570=( GEOMETRIC_REPRESENTATION_CONTEXT ( 3 ) GLOBAL_UNCERTAINTY_ASSIGNED_CONTEXT ( ( #19636 ) ) GLOBAL_UNIT_ASSIGNED_CONTEXT ( ( #9297, #18768, #2900 ) ) REPRESENTATION_CONTEXT ( 'NONE', 'WORKASPACE' ) );
#7574=ORIENTED_EDGE ( 'NONE', *, *, #8372, .F. ) ;
#7581=( GEOMETRIC_REPRESENTATION_CONTEXT ( 3 ) GLOBAL_UNCERTAINTY_ASSIGNED_CONTEXT ( ( #18004 ) ) GLOBAL_UNIT_ASSIGNED_CONTEXT ( ( #8674, #5797, #2373 ) ) REPRESENTATION_CONTEXT ( 'NONE', 'WORKASPACE' ) );
#7583=FACE_OUTER_BOUND ( 'NONE', #4678, .T. ) ;
#7607=EDGE_CURVE ( 'NONE', #4620, #20287, #14846, .T. ) ;
#7608=VERTEX_POINT ( 'NONE', #19771 ) ;
#7612=CARTESIAN_POINT ( 'NONE',  ( 133.4893729001365728, 167.9162550801369491, -97.94896630388704750 ) ) ;
#7615=CARTESIAN_POINT ( 'NONE',  ( 53.48937290013660828, 34.32473510485366575, 250.0000000000000000 ) ) ;
#7619=EDGE_CURVE ( 'NONE', #21, #7608, #5676, .T. ) ;
#7633=DIRECTION ( 'NONE',  ( -1.000000000000000000, -2.135044278125301096E-16, -0.000000000000000000 ) ) ;
#7646=AXIS2_PLACEMENT_3D ( 'NONE', #2103, #569, #6877 ) ;
#7662=AXIS2_PLACEMENT_3D ( 'NONE', #11781, #9925, #13231 ) ;
#7686=CARTESIAN_POINT ( 'NONE',  ( -211.5106270998635409, 113.1299228374912502, 29.36128450348865471 ) ) ;
#7691=COLOUR_RGB ( '', 0.08235294, 0.09019608, 0.10196078) ;
#7699=SURFACE_STYLE_FILL_AREA ( #10582 ) ;
#7702=CIRCLE ( 'NONE', #4748, 10.00000000000000888 ) ;
#7707=VECTOR ( 'NONE', #13884, 1000.000000000000000 ) ;
#7710=EDGE_CURVE ( 'NONE', #2115, #198, #15785, .T. ) ;
#7711=VECTOR ( 'NONE', #348, 1000.000000000000000 ) ;
#7712=ORIENTED_EDGE ( 'NONE', *, *, #19202, .F. ) ;
#7722=CARTESIAN_POINT ( 'NONE',  ( 143.0892156028631348, 80.91625508013694912, 245.0000000000000000 ) ) ;
#7728=VECTOR ( 'NONE', #531, 1000.000000000000000 ) ;
#7741=VECTOR ( 'NONE', #9744, 1000.000000000000000 ) ;
#7756=CARTESIAN_POINT ( 'NONE',  ( 88.88953019741013861, 167.9162550801369491, 245.0000000000000000 ) ) ;
#7759=EDGE_CURVE ( 'NONE', #530, #10424, #12577, .T. ) ;
#7766=PRESENTATION_STYLE_ASSIGNMENT (( #4975 ) ) ;
#7770=( NAMED_UNIT ( * ) SI_UNIT ( $, .STERADIAN. ) SOLID_ANGLE_UNIT ( ) );
#7773=VECTOR ( 'NONE', #8488, 1000.000000000000000 ) ;
#7777=ORIENTED_EDGE ( 'NONE', *, *, #11378, .T. ) ;
#7785=ORIENTED_EDGE ( 'NONE', *, *, #16182, .T. ) ;
#7788=VERTEX_POINT ( 'NONE', #10937 ) ;
#7801=DIRECTION ( 'NONE',  ( -0.000000000000000000, -0.000000000000000000, 1.000000000000000000 ) ) ;
#7847=DIRECTION ( 'NONE',  ( 1.000000000000000000, 5.889072920838430686E-16, -0.000000000000000000 ) ) ;
#7848=STYLED_ITEM ( 'NONE', ( #3774 ), #4833 ) ;
#7858=CYLINDRICAL_SURFACE ( 'NONE', #19569, 10.00000000000000888 ) ;
#7871=ORIENTED_EDGE ( 'NONE', *, *, #4475, .F. ) ;
#7875=ORIENTED_EDGE ( 'NONE', *, *, #14201, .F. ) ;
#7879=CARTESIAN_POINT ( 'NONE',  ( 98.48937290013660117, 80.91625508013694912, -97.94896630388704750 ) ) ;
#7882=DIRECTION ( 'NONE',  ( 1.000000000000000000, 0.000000000000000000, 0.000000000000000000 ) ) ;
#7893=DIRECTION ( 'NONE',  ( 0.000000000000000000, -1.000000000000000000, 0.000000000000000000 ) ) ;
#7907=AXIS2_PLACEMENT_3D ( 'NONE', #9627, #17366, #6352 ) ;
#7916=( NAMED_UNIT ( * ) SI_UNIT ( $, .STERADIAN. ) SOLID_ANGLE_UNIT ( ) );
#7927=ORIENTED_EDGE ( 'NONE', *, *, #16834, .F. ) ;
#7930=LINE ( 'NONE', #2976, #4773 ) ;
#7932=ORIENTED_EDGE ( 'NONE', *, *, #15550, .T. ) ;
#7953=EDGE_LOOP ( 'NONE', ( #8011, #11, #3630, #19091, #17526, #6816, #2079, #17232 ) ) ;
#7955=CARTESIAN_POINT ( 'NONE',  ( 98.48937290013662960, 103.1299228374914208, 170.4174721992565082 ) ) ;
#7965=DIRECTION ( 'NONE',  ( 1.000000000000000000, 5.889072920838430686E-16, -0.000000000000000000 ) ) ;
#7969=EDGE_CURVE ( 'NONE', #4687, #6099, #8853, .T. ) ;
#7971=DIRECTION ( 'NONE',  ( 1.000000000000000000, 0.000000000000000000, 0.000000000000000000 ) ) ;
#7974=STYLED_ITEM ( 'NONE', ( #16963 ), #17786 ) ;
#7980=CIRCLE ( 'NONE', #6002, 10.00000000000000888 ) ;
#7988=( NAMED_UNIT ( * ) PLANE_ANGLE_UNIT ( ) SI_UNIT ( $, .RADIAN. ) );
#7990=DIRECTION ( 'NONE',  ( 1.000000000000000000, 5.889072920838430686E-16, -0.000000000000000000 ) ) ;
#7993=DIRECTION ( 'NONE',  ( 0.000000000000000000, 1.000000000000000000, 0.000000000000000000 ) ) ;
#7998=CARTESIAN_POINT ( 'NONE',  ( 98.48937290013662960, 113.1299228374914350, 29.36128450348865471 ) ) ;
#8008=DIRECTION ( 'NONE',  ( -1.000000000000000000, 0.000000000000000000, -0.000000000000000000 ) ) ;
#8011=ORIENTED_EDGE ( 'NONE', *, *, #598, .T. ) ;
#8015=DIRECTION ( 'NONE',  ( 0.000000000000000000, 1.000000000000000000, 0.000000000000000000 ) ) ;
#8025=STYLED_ITEM ( 'NONE', ( #9850 ), #18911 ) ;
#8030=PLANE ( 'NONE',  #6911 ) ;
#8037=ADVANCED_FACE ( 'NONE', ( #9246 ), #182, .F. ) ;
#8053=CARTESIAN_POINT ( 'NONE',  ( 0.000000000000000000, 145.9162550801369491, 250.0000000000000000 ) ) ;
#8056=LINE ( 'NONE', #7756, #10031 ) ;
#8059=( LENGTH_UNIT ( ) NAMED_UNIT ( * ) SI_UNIT ( .MILLI., .METRE. ) );
#8073=FILL_AREA_STYLE_COLOUR ( '', #19866 ) ;
#8104=DIRECTION ( 'NONE',  ( 0.000000000000000000, 1.000000000000000000, 0.000000000000000000 ) ) ;
#8115=CARTESIAN_POINT ( 'NONE',  ( 53.48937290013658696, 123.1299228374914065, 29.36128450348865471 ) ) ;
#8120=VERTEX_POINT ( 'NONE', #8130 ) ;
#8122=EDGE_CURVE ( 'NONE', #2876, #3672, #14400, .T. ) ;
#8126=CARTESIAN_POINT ( 'NONE',  ( 153.4893729001366864, 113.1299228374914634, 29.36128450348865471 ) ) ;
#8128=CARTESIAN_POINT ( 'NONE',  ( -211.5106270998635409, 113.1299228374912502, 170.4174721992565082 ) ) ;
#8130=CARTESIAN_POINT ( 'NONE',  ( 82.88953019741013861, 167.9162550801369491, 250.0000000000000000 ) ) ;
#8136=EDGE_CURVE ( 'NONE', #10467, #17875, #16231, .T. ) ;
#8142=CARTESIAN_POINT ( 'NONE',  ( 53.48937290013658696, 113.1299228374914065, 220.6387154965113382 ) ) ;
#8153=CARTESIAN_POINT ( 'NONE',  ( 153.4893729001366864, 113.1299228374914634, 170.4174721992565082 ) ) ;
#8160=FACE_OUTER_BOUND ( 'NONE', #7532, .T. ) ;
#8163=CARTESIAN_POINT ( 'NONE',  ( 78.48937290013660117, 145.9162550801369491, 0.000000000000000000 ) ) ;
#8173=ORIENTED_EDGE ( 'NONE', *, *, #9585, .T. ) ;
#8174=CARTESIAN_POINT ( 'NONE',  ( 0.000000000000000000, 80.91625508013694912, 0.000000000000000000 ) ) ;
#8192=CARTESIAN_POINT ( 'NONE',  ( 133.4893729001365443, 103.1299228374914492, 220.6387154965113382 ) ) ;
#8196=EDGE_LOOP ( 'NONE', ( #3534, #11742, #10662, #7516 ) ) ;
#8200=VERTEX_POINT ( 'NONE', #16869 ) ;
#8222=CIRCLE ( 'NONE', #10182, 10.00000000000000888 ) ;
#8231=CARTESIAN_POINT ( 'NONE',  ( 78.48937290013660117, 103.1299228374914065, 79.58252780074349175 ) ) ;
#8234=DIRECTION ( 'NONE',  ( 1.000000000000000000, 0.000000000000000000, 0.000000000000000000 ) ) ;
#8252=AXIS2_PLACEMENT_3D ( 'NONE', #11752, #16492, #13498 ) ;
#8268=ORIENTED_EDGE ( 'NONE', *, *, #1076, .F. ) ;
#8270=( NAMED_UNIT ( * ) PLANE_ANGLE_UNIT ( ) SI_UNIT ( $, .RADIAN. ) );
#8272=UNCERTAINTY_MEASURE_WITH_UNIT (LENGTH_MEASURE( 1.000000000000000082E-05 ), #16448, 'distance_accuracy_value', 'NONE');
#8296=( NAMED_UNIT ( * ) SI_UNIT ( $, .STERADIAN. ) SOLID_ANGLE_UNIT ( ) );
#8298=ORIENTED_EDGE ( 'NONE', *, *, #15928, .T. ) ;
#8301=FACE_OUTER_BOUND ( 'NONE', #19466, .T. ) ;
#8305=LINE ( 'NONE', #1985, #4040 ) ;
#8307=CARTESIAN_POINT ( 'NONE',  ( -211.5106270998635409, 123.1299228374912644, 170.4174721992565082 ) ) ;
#8342=DIRECTION ( 'NONE',  ( 0.000000000000000000, -1.000000000000000000, 0.000000000000000000 ) ) ;
#8347=ORIENTED_EDGE ( 'NONE', *, *, #18438, .F. ) ;
#8356=DIRECTION ( 'NONE',  ( 0.000000000000000000, 0.000000000000000000, -1.000000000000000000 ) ) ;
#8362=EDGE_CURVE ( 'NONE', #13442, #16217, #4356, .T. ) ;
#8372=EDGE_CURVE ( 'NONE', #6099, #14468, #9842, .T. ) ;
#8379=FILL_AREA_STYLE ('',( #9919 ) ) ;
#8382=EDGE_CURVE ( 'NONE', #14402, #13737, #8305, .T. ) ;
#8386=( NAMED_UNIT ( * ) SI_UNIT ( $, .STERADIAN. ) SOLID_ANGLE_UNIT ( ) );
#8393=DIRECTION ( 'NONE',  ( 0.000000000000000000, 0.000000000000000000, -1.000000000000000000 ) ) ;
#8408=( LENGTH_UNIT ( ) NAMED_UNIT ( * ) SI_UNIT ( .MILLI., .METRE. ) );
#8421=FILL_AREA_STYLE ('',( #862 ) ) ;
#8436=ORIENTED_EDGE ( 'NONE', *, *, #14342, .T. ) ;
#8448=SURFACE_STYLE_FILL_AREA ( #11526 ) ;
#8457=AXIS2_PLACEMENT_3D ( 'NONE', #8126, #14297, #19012 ) ;
#8465=DIRECTION ( 'NONE',  ( -0.000000000000000000, -1.000000000000000000, -0.000000000000000000 ) ) ;
#8468=ORIENTED_EDGE ( 'NONE', *, *, #12073, .F. ) ;
#8473=CARTESIAN_POINT ( 'NONE',  ( 82.88953019741013861, 80.91625508013694912, 245.0000000000000000 ) ) ;
#8474=FACE_OUTER_BOUND ( 'NONE', #15185, .T. ) ;
#8476=DIRECTION ( 'NONE',  ( -1.000000000000000000, -1.595148023886719315E-16, 0.000000000000000000 ) ) ;
#8480=( NAMED_UNIT ( * ) SI_UNIT ( $, .STERADIAN. ) SOLID_ANGLE_UNIT ( ) );
#8488=DIRECTION ( 'NONE',  ( 2.135044278125300850E-16, -1.000000000000000000, 0.000000000000000000 ) ) ;
#8489=EDGE_CURVE ( 'NONE', #3093, #825, #4063, .T. ) ;
#8491=FILL_AREA_STYLE_COLOUR ( '', #16283 ) ;
#8494=ADVANCED_FACE ( 'NONE', ( #19695 ), #13458, .F. ) ;
#8500=ORIENTED_EDGE ( 'NONE', *, *, #8372, .T. ) ;
#8516=DIRECTION ( 'NONE',  ( -1.000000000000000000, -1.595148023886719315E-16, 0.000000000000000000 ) ) ;
#8517=ORIENTED_EDGE ( 'NONE', *, *, #15801, .F. ) ;
#8526=UNCERTAINTY_MEASURE_WITH_UNIT (LENGTH_MEASURE( 1.000000000000000082E-05 ), #1369, 'distance_accuracy_value', 'NONE');
#8528=SURFACE_STYLE_USAGE ( .BOTH. , #16395 ) ;
#8534=STYLED_ITEM ( 'NONE', ( #18621 ), #5523 ) ;
#8559=CARTESIAN_POINT ( 'NONE',  ( 153.4893729001366864, 123.1299228374914634, 170.4174721992565082 ) ) ;
#8564=CARTESIAN_POINT ( 'NONE',  ( -211.5106270998635409, 113.1299228374912502, 170.4174721992565082 ) ) ;
#8565=DIRECTION ( 'NONE',  ( 0.000000000000000000, 0.000000000000000000, 1.000000000000000000 ) ) ;
#8571=( LENGTH_UNIT ( ) NAMED_UNIT ( * ) SI_UNIT ( .MILLI., .METRE. ) );
#8573=VECTOR ( 'NONE', #14237, 1000.000000000000000 ) ;
#8581=FACE_BOUND ( 'NONE', #15305, .T. ) ;
#8584=ORIENTED_EDGE ( 'NONE', *, *, #12055, .F. ) ;
#8586=CARTESIAN_POINT ( 'NONE',  ( 178.4893729001365443, 145.9162550801369491, 0.000000000000000000 ) ) ;
#8588=UNCERTAINTY_MEASURE_WITH_UNIT (LENGTH_MEASURE( 1.000000000000000082E-05 ), #3762, 'distance_accuracy_value', 'NONE');
#8597=PLANE ( 'NONE',  #5709 ) ;
#8623=DIRECTION ( 'NONE',  ( -1.000000000000000000, 0.000000000000000000, -0.000000000000000000 ) ) ;
#8626=( LENGTH_UNIT ( ) NAMED_UNIT ( * ) SI_UNIT ( .MILLI., .METRE. ) );
#8628=CARTESIAN_POINT ( 'NONE',  ( 153.4893729001366864, 123.1299228374914634, 220.6387154965113382 ) ) ;
#8633=VERTEX_POINT ( 'NONE', #5233 ) ;
#8636=PRODUCT_DEFINITION_CONTEXT ( 'detailed design', #11975, 'design' ) ;
#8645=VECTOR ( 'NONE', #19216, 1000.000000000000000 ) ;
#8655=VECTOR ( 'NONE', #5750, 1000.000000000000000 ) ;
#8663=ORIENTED_EDGE ( 'NONE', *, *, #2961, .T. ) ;
#8668=STYLED_ITEM ( 'NONE', ( #9277 ), #14002 ) ;
#8673=UNCERTAINTY_MEASURE_WITH_UNIT (LENGTH_MEASURE( 1.000000000000000082E-05 ), #2988, 'distance_accuracy_value', 'NONE');
#8674=( LENGTH_UNIT ( ) NAMED_UNIT ( * ) SI_UNIT ( .MILLI., .METRE. ) );
#8680=DIRECTION ( 'NONE',  ( 0.000000000000000000, 0.000000000000000000, 1.000000000000000000 ) ) ;
#8681=( LENGTH_UNIT ( ) NAMED_UNIT ( * ) SI_UNIT ( .MILLI., .METRE. ) );
#8683=EDGE_LOOP ( 'NONE', ( #16003, #16464, #201, #7927 ) ) ;
#8686=MECHANICAL_DESIGN_GEOMETRIC_PRESENTATION_REPRESENTATION('',(#19531),#7063);
#8700=FACE_BOUND ( 'NONE', #16254, .T. ) ;
#8709=FILL_AREA_STYLE ('',( #19609 ) ) ;
#8716=FACE_OUTER_BOUND ( 'NONE', #4578, .T. ) ;
#8727=EDGE_CURVE ( 'NONE', #19572, #8200, #15205, .T. ) ;
#8739=CARTESIAN_POINT ( 'NONE',  ( 53.48937290013659407, 145.9162550801369491, 250.0000000000000000 ) ) ;
#8745=DIRECTION ( 'NONE',  ( -1.000000000000000000, 0.000000000000000000, 0.000000000000000000 ) ) ;
#8756=EDGE_CURVE ( 'NONE', #12453, #17418, #11821, .T. ) ;
#8760=CARTESIAN_POINT ( 'NONE',  ( 0.000000000000000000, 145.9162550801369491, 250.0000000000000000 ) ) ;
#8761=DIRECTION ( 'NONE',  ( -1.000000000000000000, -0.000000000000000000, -0.000000000000000000 ) ) ;
#8766=CARTESIAN_POINT ( 'NONE',  ( 78.48937290013660117, 103.1299228374914065, 220.6387154965113382 ) ) ;
#8767=DIRECTION ( 'NONE',  ( 0.000000000000000000, 1.000000000000000000, 0.000000000000000000 ) ) ;
#8775=AXIS2_PLACEMENT_3D ( 'NONE', #18417, #19960, #12359 ) ;
#8780=DIRECTION ( 'NONE',  ( 0.000000000000000000, -1.000000000000000000, 0.000000000000000000 ) ) ;
#8784=( NAMED_UNIT ( * ) SI_UNIT ( $, .STERADIAN. ) SOLID_ANGLE_UNIT ( ) );
#8789=LINE ( 'NONE', #17676, #19818 ) ;
#8790=EDGE_CURVE ( 'NONE', #7147, #270, #16678, .T. ) ;
#8799=EDGE_CURVE ( 'NONE', #3886, #15108, #5734, .T. ) ;
#8800=ORIENTED_EDGE ( 'NONE', *, *, #14106, .F. ) ;
#8801=EDGE_LOOP ( 'NONE', ( #12112, #9576 ) ) ;
#8823=ORIENTED_EDGE ( 'NONE', *, *, #16650, .F. ) ;
#8827=DIRECTION ( 'NONE',  ( 1.000000000000000000, 5.889072920838430686E-16, -0.000000000000000000 ) ) ;
#8831=CARTESIAN_POINT ( 'NONE',  ( 153.4893729001366580, 145.9162550801369491, 250.0000000000000000 ) ) ;
#8840=FACE_OUTER_BOUND ( 'NONE', #445, .T. ) ;
#8841=DIRECTION ( 'NONE',  ( -0.000000000000000000, 0.000000000000000000, 1.000000000000000000 ) ) ;
#8842=COLOUR_RGB ( '', 0.72549020, 0.75294118, 0.79215686) ;
#8845=ORIENTED_EDGE ( 'NONE', *, *, #12080, .F. ) ;
#8847=EDGE_LOOP ( 'NONE', ( #12945, #16050, #20215, #13495 ) ) ;
#8849=EDGE_CURVE ( 'NONE', #3093, #5899, #19277, .T. ) ;
#8850=LINE ( 'NONE', #2655, #7707 ) ;
#8853=LINE ( 'NONE', #13702, #14266 ) ;
#8854=CYLINDRICAL_SURFACE ( 'NONE', #14611, 10.00000000000000888 ) ;
#8856=CARTESIAN_POINT ( 'NONE',  ( -211.5106270998635409, 113.1299228374912502, 79.58252780074349175 ) ) ;
#8857=PRESENTATION_STYLE_ASSIGNMENT (( #7221 ) ) ;
#8864=ORIENTED_EDGE ( 'NONE', *, *, #13819, .T. ) ;
#8869=UNCERTAINTY_MEASURE_WITH_UNIT (LENGTH_MEASURE( 1.000000000000000082E-05 ), #17878, 'distance_accuracy_value', 'NONE');
#8885=DIRECTION ( 'NONE',  ( 0.000000000000000000, 0.000000000000000000, 1.000000000000000000 ) ) ;
#8891=UNCERTAINTY_MEASURE_WITH_UNIT (LENGTH_MEASURE( 1.000000000000000082E-05 ), #7145, 'distance_accuracy_value', 'NONE');
#8898=PRESENTATION_STYLE_ASSIGNMENT (( #11900 ) ) ;
#8902=MECHANICAL_DESIGN_GEOMETRIC_PRESENTATION_REPRESENTATION('',(#20064),#18761);
#8906=DIRECTION ( 'NONE',  ( 0.000000000000000000, 1.000000000000000000, 0.000000000000000000 ) ) ;
#8914=EDGE_CURVE ( 'NONE', #2877, #1858, #10667, .T. ) ;
#8921=CYLINDRICAL_SURFACE ( 'NONE', #12864, 10.00000000000000888 ) ;
#8943=CARTESIAN_POINT ( 'NONE',  ( 153.4893729001366864, 123.1299228374914634, 29.36128450348865471 ) ) ;
#8944=DIRECTION ( 'NONE',  ( 0.000000000000000000, 0.000000000000000000, 1.000000000000000000 ) ) ;
#8945=SURFACE_STYLE_USAGE ( .BOTH. , #18522 ) ;
#8955=VECTOR ( 'NONE', #17084, 1000.000000000000000 ) ;
#8967=AXIS2_PLACEMENT_3D ( 'NONE', #3640, #16338, #11250 ) ;
#8969=FACE_OUTER_BOUND ( 'NONE', #16627, .T. ) ;
#8997=EDGE_CURVE ( 'NONE', #17019, #16028, #11173, .T. ) ;
#9000=DIRECTION ( 'NONE',  ( -0.000000000000000000, -0.000000000000000000, 1.000000000000000000 ) ) ;
#9017=( GEOMETRIC_REPRESENTATION_CONTEXT ( 3 ) GLOBAL_UNCERTAINTY_ASSIGNED_CONTEXT ( ( #14657 ) ) GLOBAL_UNIT_ASSIGNED_CONTEXT ( ( #14861, #726, #8386 ) ) REPRESENTATION_CONTEXT ( 'NONE', 'WORKASPACE' ) );
#9023=AXIS2_PLACEMENT_3D ( 'NONE', #836, #2490, #2582 ) ;
#9059=CIRCLE ( 'NONE', #6112, 10.00000000000000888 ) ;
#9065=CARTESIAN_POINT ( 'NONE',  ( 133.4893729001365443, 113.1299228374914634, 29.36128450348865471 ) ) ;
#9069=LINE ( 'NONE', #1094, #11635 ) ;
#9070=CARTESIAN_POINT ( 'NONE',  ( 133.4893729001365728, 80.91625508013694912, 250.0000000000000000 ) ) ;
#9072=EDGE_CURVE ( 'NONE', #5614, #1681, #4586, .T. ) ;
#9082=DIRECTION ( 'NONE',  ( 0.000000000000000000, -1.000000000000000000, 0.000000000000000000 ) ) ;
#9101=ORIENTED_EDGE ( 'NONE', *, *, #10147, .T. ) ;
#9106=CIRCLE ( 'NONE', #11422, 10.00000000000000888 ) ;
#9122=VERTEX_POINT ( 'NONE', #11386 ) ;
#9144=VECTOR ( 'NONE', #8623, 1000.000000000000000 ) ;
#9153=DIRECTION ( 'NONE',  ( 0.000000000000000000, 1.000000000000000000, 0.000000000000000000 ) ) ;
#9154=ORIENTED_EDGE ( 'NONE', *, *, #10541, .F. ) ;
#9165=STYLED_ITEM ( 'NONE', ( #14762 ), #5022 ) ;
#9174=PLANE ( 'NONE',  #9994 ) ;
#9183=PRESENTATION_STYLE_ASSIGNMENT (( #9401 ) ) ;
#9186=EDGE_CURVE ( 'NONE', #10424, #14402, #2188, .T. ) ;
#9189=STYLED_ITEM ( 'NONE', ( #18998 ), #10903 ) ;
#9193=ORIENTED_EDGE ( 'NONE', *, *, #9602, .T. ) ;
#9197=DIRECTION ( 'NONE',  ( 0.000000000000000000, 1.000000000000000000, -0.000000000000000000 ) ) ;
#9201=CARTESIAN_POINT ( 'NONE',  ( -211.5106270998635409, 113.1299228374912502, 29.36128450348865471 ) ) ;
#9206=VECTOR ( 'NONE', #19255, 1000.000000000000000 ) ;
#9212=EDGE_LOOP ( 'NONE', ( #16956, #12036, #19617, #14866 ) ) ;
#9216=EDGE_LOOP ( 'NONE', ( #19350, #12258, #10049, #2147 ) ) ;
#9224=CARTESIAN_POINT ( 'NONE',  ( -211.5106270998635409, 103.1299228374912360, 170.4174721992565082 ) ) ;
#9226=CARTESIAN_POINT ( 'NONE',  ( 143.0892156028631348, 167.9162550801369491, 250.0000000000000000 ) ) ;
#9230=CARTESIAN_POINT ( 'NONE',  ( 98.48937290013662960, 113.1299228374914350, 29.36128450348865471 ) ) ;
#9246=FACE_OUTER_BOUND ( 'NONE', #16247, .T. ) ;
#9251=AXIS2_PLACEMENT_3D ( 'NONE', #5986, #4156, #12082 ) ;
#9255=FACE_OUTER_BOUND ( 'NONE', #5050, .T. ) ;
#9265=ORIENTED_EDGE ( 'NONE', *, *, #18188, .T. ) ;
#9274=FILL_AREA_STYLE ('',( #4857 ) ) ;
#9277=PRESENTATION_STYLE_ASSIGNMENT (( #18546 ) ) ;
#9297=( LENGTH_UNIT ( ) NAMED_UNIT ( * ) SI_UNIT ( .MILLI., .METRE. ) );
#9313=CARTESIAN_POINT ( 'NONE',  ( 149.0892156028631348, 80.91625508013694912, 245.0000000000000000 ) ) ;
#9329=DIRECTION ( 'NONE',  ( 0.000000000000000000, -1.000000000000000000, 0.000000000000000000 ) ) ;
#9334=EDGE_LOOP ( 'NONE', ( #5857, #8663 ) ) ;
#9342=VECTOR ( 'NONE', #13628, 1000.000000000000000 ) ;
#9352=PLANE ( 'NONE',  #5819 ) ;
#9355=CARTESIAN_POINT ( 'NONE',  ( 153.4893729001366864, 113.1299228374914634, 220.6387154965113382 ) ) ;
#9357=ORIENTED_EDGE ( 'NONE', *, *, #3518, .T. ) ;
#9372=MECHANICAL_DESIGN_GEOMETRIC_PRESENTATION_REPRESENTATION('',(#6088),#11026);
#9385=EDGE_CURVE ( 'NONE', #3638, #1247, #2677, .T. ) ;
#9394=EDGE_CURVE ( 'NONE', #7608, #6545, #17021, .T. ) ;
#9398=VECTOR ( 'NONE', #9000, 1000.000000000000000 ) ;
#9401=SURFACE_STYLE_USAGE ( .BOTH. , #1746 ) ;
#9432=CARTESIAN_POINT ( 'NONE',  ( 88.88953019741013861, 80.91625508013694912, 250.0000000000000000 ) ) ;
#9436=( NAMED_UNIT ( * ) SI_UNIT ( $, .STERADIAN. ) SOLID_ANGLE_UNIT ( ) );
#9454=VERTEX_POINT ( 'NONE', #3513 ) ;
#9455=CARTESIAN_POINT ( 'NONE',  ( -211.5106270998635409, 123.1299228374912644, 79.58252780074349175 ) ) ;
#9477=( NAMED_UNIT ( * ) SI_UNIT ( $, .STERADIAN. ) SOLID_ANGLE_UNIT ( ) );
#9480=SURFACE_STYLE_FILL_AREA ( #9274 ) ;
#9482=LINE ( 'NONE', #17926, #16591 ) ;
#9525=PRESENTATION_STYLE_ASSIGNMENT (( #254 ) ) ;
#9529=CARTESIAN_POINT ( 'NONE',  ( 178.4893729001366012, 34.32473510485366575, 0.000000000000000000 ) ) ;
#9543=VECTOR ( 'NONE', #191, 1000.000000000000000 ) ;
#9544=CIRCLE ( 'NONE', #8252, 10.00000000000000888 ) ;
#9562=DIRECTION ( 'NONE',  ( 1.000000000000000000, -0.000000000000000000, 0.000000000000000000 ) ) ;
#9563=EDGE_CURVE ( 'NONE', #10819, #6194, #19603, .T. ) ;
#9576=ORIENTED_EDGE ( 'NONE', *, *, #16790, .T. ) ;
#9580=ORIENTED_EDGE ( 'NONE', *, *, #16182, .F. ) ;
#9582=CYLINDRICAL_SURFACE ( 'NONE', #5748, 10.00000000000000888 ) ;
#9585=EDGE_CURVE ( 'NONE', #3302, #1869, #3708, .T. ) ;
#9587=FILL_AREA_STYLE_COLOUR ( '', #12542 ) ;
#9590=( GEOMETRIC_REPRESENTATION_CONTEXT ( 3 ) GLOBAL_UNCERTAINTY_ASSIGNED_CONTEXT ( ( #20190 ) ) GLOBAL_UNIT_ASSIGNED_CONTEXT ( ( #864, #19813, #7080 ) ) REPRESENTATION_CONTEXT ( 'NONE', 'WORKASPACE' ) );
#9602=EDGE_CURVE ( 'NONE', #4977, #10759, #17972, .T. ) ;
#9604=FACE_OUTER_BOUND ( 'NONE', #8196, .T. ) ;
#9620=CIRCLE ( 'NONE', #10614, 10.00000000000000888 ) ;
#9622=FILL_AREA_STYLE_COLOUR ( '', #17801 ) ;
#9624=ADVANCED_FACE ( 'NONE', ( #12452, #19953, #12137, #18319, #12351 ), #9352, .F. ) ;
#9627=CARTESIAN_POINT ( 'NONE',  ( 78.48937290013661539, 80.91625508013694912, -140.0000000000001137 ) ) ;
#9645=ORIENTED_EDGE ( 'NONE', *, *, #5353, .T. ) ;
#9694=CARTESIAN_POINT ( 'NONE',  ( 153.4893729001366580, 80.91625508013694912, -140.0000000000001137 ) ) ;
#9703=CIRCLE ( 'NONE', #2114, 10.00000000000000888 ) ;
#9723=DIRECTION ( 'NONE',  ( 1.000000000000000000, -0.000000000000000000, 0.000000000000000000 ) ) ;
#9735=EDGE_CURVE ( 'NONE', #1869, #5907, #10420, .T. ) ;
#9736=EDGE_LOOP ( 'NONE', ( #17146, #18032 ) ) ;
#9744=DIRECTION ( 'NONE',  ( 1.000000000000000000, 5.889072920838430686E-16, -0.000000000000000000 ) ) ;
#9746=DIRECTION ( 'NONE',  ( -0.000000000000000000, -0.000000000000000000, -1.000000000000000000 ) ) ;
#9778=DIRECTION ( 'NONE',  ( 1.000000000000000000, 0.000000000000000000, 0.000000000000000000 ) ) ;
#9784=DIRECTION ( 'NONE',  ( 0.000000000000000000, 1.000000000000000000, 0.000000000000000000 ) ) ;
#9789=ORIENTED_EDGE ( 'NONE', *, *, #8136, .F. ) ;
#9797=DIRECTION ( 'NONE',  ( 0.000000000000000000, 1.000000000000000000, 0.000000000000000000 ) ) ;
#9801=LINE ( 'NONE', #9694, #785 ) ;
#9804=EDGE_CURVE ( 'NONE', #9122, #6311, #9106, .T. ) ;
#9814=PRESENTATION_STYLE_ASSIGNMENT (( #3426 ) ) ;
#9815=EDGE_LOOP ( 'NONE', ( #19511, #16194 ) ) ;
#9819=FACE_BOUND ( 'NONE', #5733, .T. ) ;
#9821=DIRECTION ( 'NONE',  ( 1.000000000000000000, 5.889072920838430686E-16, -0.000000000000000000 ) ) ;
#9827=FILL_AREA_STYLE_COLOUR ( '', #5555 ) ;
#9837=( GEOMETRIC_REPRESENTATION_CONTEXT ( 3 ) GLOBAL_UNCERTAINTY_ASSIGNED_CONTEXT ( ( #449 ) ) GLOBAL_UNIT_ASSIGNED_CONTEXT ( ( #13048, #437, #3645 ) ) REPRESENTATION_CONTEXT ( 'NONE', 'WORKASPACE' ) );
#9839=PRESENTATION_STYLE_ASSIGNMENT (( #17866 ) ) ;
#9842=LINE ( 'NONE', #16156, #11945 ) ;
#9850=PRESENTATION_STYLE_ASSIGNMENT (( #19615 ) ) ;
#9860=APPLICATION_CONTEXT ( 'automotive_design' ) ;
#9883=ORIENTED_EDGE ( 'NONE', *, *, #9072, .T. ) ;
#9906=CARTESIAN_POINT ( 'NONE',  ( 153.4893729001366864, 123.1299228374914634, 220.6387154965113382 ) ) ;
#9915=CYLINDRICAL_SURFACE ( 'NONE', #10674, 10.00000000000000888 ) ;
#9917=UNCERTAINTY_MEASURE_WITH_UNIT (LENGTH_MEASURE( 1.000000000000000082E-05 ), #7237, 'distance_accuracy_value', 'NONE');
#9918=ORIENTED_EDGE ( 'NONE', *, *, #10094, .F. ) ;
#9919=FILL_AREA_STYLE_COLOUR ( '', #14669 ) ;
#9920=SURFACE_SIDE_STYLE ('',( #13039 ) ) ;
#9923=SURFACE_STYLE_USAGE ( .BOTH. , #11367 ) ;
#9925=DIRECTION ( 'NONE',  ( -1.000000000000000000, 0.000000000000000000, 0.000000000000000000 ) ) ;
#9926=CYLINDRICAL_SURFACE ( 'NONE', #15986, 10.00000000000000888 ) ;
#9931=SURFACE_STYLE_FILL_AREA ( #335 ) ;
#9940=ORIENTED_EDGE ( 'NONE', *, *, #805, .T. ) ;
#9942=CARTESIAN_POINT ( 'NONE',  ( 78.48937290013662960, 1.675782865040797740E-14, -97.94896630388704750 ) ) ;
#9945=DIRECTION ( 'NONE',  ( 1.000000000000000000, 0.000000000000000000, 0.000000000000000000 ) ) ;
#9951=FACE_OUTER_BOUND ( 'NONE', #2603, .T. ) ;
#9952=CARTESIAN_POINT ( 'NONE',  ( 133.4893729001365443, 113.1299228374914634, 79.58252780074349175 ) ) ;
#9967=AXIS2_PLACEMENT_3D ( 'NONE', #14477, #6965, #8104 ) ;
#9973=CARTESIAN_POINT ( 'NONE',  ( -211.5106270998635409, 103.1299228374912360, 220.6387154965113382 ) ) ;
#9975=CARTESIAN_POINT ( 'NONE',  ( 0.000000000000000000, 80.91625508013694912, 250.0000000000000000 ) ) ;
#9979=CARTESIAN_POINT ( 'NONE',  ( 0.000000000000000000, 0.000000000000000000, 250.0000000000000000 ) ) ;
#9983=ORIENTED_EDGE ( 'NONE', *, *, #12055, .T. ) ;
#9986=CLOSED_SHELL ( 'NONE', ( #12925, #736, #4868, #2897, #6193, #16557, #10768, #5523, #5969, #19198, #4856, #10258, #10481, #6937, #10527, #553, #7367, #13510, #19042, #15306 ) ) ;
#9988=VECTOR ( 'NONE', #1398, 1000.000000000000000 ) ;
#9994=AXIS2_PLACEMENT_3D ( 'NONE', #4446, #15788, #11044 ) ;
#10002=VECTOR ( 'NONE', #13364, 1000.000000000000000 ) ;
#10004=STYLED_ITEM ( 'NONE', ( #6202 ), #343 ) ;
#10020=CARTESIAN_POINT ( 'NONE',  ( 153.4893729001366864, 123.1299228374914634, 79.58252780074349175 ) ) ;
#10028=VECTOR ( 'NONE', #18449, 1000.000000000000000 ) ;
#10031=VECTOR ( 'NONE', #312, 1000.000000000000000 ) ;
#10049=ORIENTED_EDGE ( 'NONE', *, *, #7423, .F. ) ;
#10050=SURFACE_SIDE_STYLE ('',( #3560 ) ) ;
#10056=SURFACE_SIDE_STYLE ('',( #5316 ) ) ;
#10063=AXIS2_PLACEMENT_3D ( 'NONE', #11569, #5392, #8680 ) ;
#10084=DIRECTION ( 'NONE',  ( -1.000000000000000000, 0.000000000000000000, -0.000000000000000000 ) ) ;
#10087=ORIENTED_EDGE ( 'NONE', *, *, #6681, .F. ) ;
#10089=FACE_OUTER_BOUND ( 'NONE', #6956, .T. ) ;
#10092=ORIENTED_EDGE ( 'NONE', *, *, #3452, .T. ) ;
#10094=EDGE_CURVE ( 'NONE', #3589, #6194, #2831, .T. ) ;
#10098=AXIS2_PLACEMENT_3D ( 'NONE', #8153, #14424, #16602 ) ;
#10118=VECTOR ( 'NONE', #900, 1000.000000000000000 ) ;
#10119=UNCERTAINTY_MEASURE_WITH_UNIT (LENGTH_MEASURE( 1.000000000000000082E-05 ), #19963, 'distance_accuracy_value', 'NONE');
#10125=EDGE_CURVE ( 'NONE', #4967, #14468, #11176, .T. ) ;
#10136=EDGE_CURVE ( 'NONE', #10482, #5907, #3246, .T. ) ;
#10141=PRESENTATION_STYLE_ASSIGNMENT (( #5212 ) ) ;
#10146=DIRECTION ( 'NONE',  ( 1.000000000000000000, 5.889072920838430686E-16, -0.000000000000000000 ) ) ;
#10147=EDGE_CURVE ( 'NONE', #738, #14419, #17262, .T. ) ;
#10150=CARTESIAN_POINT ( 'NONE',  ( 88.88953019741013861, 80.91625508013694912, 245.0000000000000000 ) ) ;
#10162=DIRECTION ( 'NONE',  ( -1.000000000000000000, -2.135044278125301096E-16, -0.000000000000000000 ) ) ;
#10163=VERTEX_POINT ( 'NONE', #11081 ) ;
#10169=STYLED_ITEM ( 'NONE', ( #5543 ), #5371 ) ;
#10174=UNCERTAINTY_MEASURE_WITH_UNIT (LENGTH_MEASURE( 1.000000000000000082E-05 ), #15376, 'distance_accuracy_value', 'NONE');
#10176=DIRECTION ( 'NONE',  ( 1.000000000000000000, 5.889072920838430686E-16, -0.000000000000000000 ) ) ;
#10177=VERTEX_POINT ( 'NONE', #250 ) ;
#10182=AXIS2_PLACEMENT_3D ( 'NONE', #17923, #18109, #16494 ) ;
#10188=DIRECTION ( 'NONE',  ( 1.000000000000000000, 2.135044278125300850E-16, -0.000000000000000000 ) ) ;
#10198=ADVANCED_FACE ( 'NONE', ( #17558, #3152, #8581, #2394, #6773 ), #13150, .F. ) ;
#10200=DIRECTION ( 'NONE',  ( -1.000000000000000000, -2.135044278125301096E-16, -0.000000000000000000 ) ) ;
#10214=DIRECTION ( 'NONE',  ( 1.595148023886719315E-16, -1.000000000000000000, 0.000000000000000000 ) ) ;
#10218=CARTESIAN_POINT ( 'NONE',  ( -211.5106270998635409, 123.1299228374912644, 79.58252780074349175 ) ) ;
#10228=EDGE_CURVE ( 'NONE', #1247, #39, #19494, .T. ) ;
#10230=ORIENTED_EDGE ( 'NONE', *, *, #819, .F. ) ;
#10240=UNCERTAINTY_MEASURE_WITH_UNIT (LENGTH_MEASURE( 1.000000000000000082E-05 ), #8408, 'distance_accuracy_value', 'NONE');
#10258=ADVANCED_FACE ( 'NONE', ( #8301 ), #2089, .T. ) ;
#10278=LINE ( 'NONE', #16783, #20108 ) ;
#10293=CIRCLE ( 'NONE', #12602, 10.00000000000000888 ) ;
#10312=ORIENTED_EDGE ( 'NONE', *, *, #2217, .T. ) ;
#10314=( GEOMETRIC_REPRESENTATION_CONTEXT ( 3 ) GLOBAL_UNCERTAINTY_ASSIGNED_CONTEXT ( ( #8673 ) ) GLOBAL_UNIT_ASSIGNED_CONTEXT ( ( #2988, #2885, #17109 ) ) REPRESENTATION_CONTEXT ( 'NONE', 'WORKASPACE' ) );
#10324=( GEOMETRIC_REPRESENTATION_CONTEXT ( 3 ) GLOBAL_UNCERTAINTY_ASSIGNED_CONTEXT ( ( #19602 ) ) GLOBAL_UNIT_ASSIGNED_CONTEXT ( ( #5486, #7040, #8296 ) ) REPRESENTATION_CONTEXT ( 'NONE', 'WORKASPACE' ) );
#10356=DIRECTION ( 'NONE',  ( 1.000000000000000000, -0.000000000000000000, 0.000000000000000000 ) ) ;
#10363=VERTEX_POINT ( 'NONE', #16655 ) ;
#10372=AXIS2_PLACEMENT_3D ( 'NONE', #9065, #18639, #2861 ) ;
#10378=VECTOR ( 'NONE', #15544, 1000.000000000000000 ) ;
#10389=CARTESIAN_POINT ( 'NONE',  ( 143.0892156028631348, 80.91625508013694912, 245.0000000000000000 ) ) ;
#10419=EDGE_LOOP ( 'NONE', ( #10954, #8268, #4547, #533 ) ) ;
#10420=CIRCLE ( 'NONE', #8457, 10.00000000000000888 ) ;
#10424=VERTEX_POINT ( 'NONE', #12404 ) ;
#10430=DIRECTION ( 'NONE',  ( 1.000000000000000000, 5.889072920838430686E-16, -0.000000000000000000 ) ) ;
#10448=( LENGTH_UNIT ( ) NAMED_UNIT ( * ) SI_UNIT ( .MILLI., .METRE. ) );
#10454=( LENGTH_UNIT ( ) NAMED_UNIT ( * ) SI_UNIT ( .MILLI., .METRE. ) );
#10465=CARTESIAN_POINT ( 'NONE',  ( 0.000000000000000000, 167.9162550801369491, 0.000000000000000000 ) ) ;
#10467=VERTEX_POINT ( 'NONE', #7955 ) ;
#10479=( NAMED_UNIT ( * ) PLANE_ANGLE_UNIT ( ) SI_UNIT ( $, .RADIAN. ) );
#10481=ADVANCED_FACE ( 'NONE', ( #10952 ), #17427, .F. ) ;
#10482=VERTEX_POINT ( 'NONE', #3535 ) ;
#10484=ORIENTED_EDGE ( 'NONE', *, *, #19210, .F. ) ;
#10485=EDGE_CURVE ( 'NONE', #18945, #1341, #17837, .T. ) ;
#10500=( NAMED_UNIT ( * ) SI_UNIT ( $, .STERADIAN. ) SOLID_ANGLE_UNIT ( ) );
#10519=UNCERTAINTY_MEASURE_WITH_UNIT (LENGTH_MEASURE( 1.000000000000000082E-05 ), #8571, 'distance_accuracy_value', 'NONE');
#10525=VECTOR ( 'NONE', #18491, 1000.000000000000000 ) ;
#10527=ADVANCED_FACE ( 'NONE', ( #11460 ), #9915, .F. ) ;
#10530=CARTESIAN_POINT ( 'NONE',  ( -211.5106270998635409, 113.1299228374912502, 220.6387154965113382 ) ) ;
#10536=VECTOR ( 'NONE', #19703, 1000.000000000000000 ) ;
#10540=ORIENTED_EDGE ( 'NONE', *, *, #4493, .T. ) ;
#10541=EDGE_CURVE ( 'NONE', #17811, #5524, #1092, .T. ) ;
#10542=SURFACE_STYLE_FILL_AREA ( #4265 ) ;
#10546=SURFACE_STYLE_FILL_AREA ( #15300 ) ;
#10563=ORIENTED_EDGE ( 'NONE', *, *, #598, .F. ) ;
#10564=ORIENTED_EDGE ( 'NONE', *, *, #16210, .F. ) ;
#10567=DIRECTION ( 'NONE',  ( -1.000000000000000000, 0.000000000000000000, 0.000000000000000000 ) ) ;
#10572=EDGE_CURVE ( 'NONE', #2877, #16599, #13888, .T. ) ;
#10575=FACE_BOUND ( 'NONE', #9815, .T. ) ;
#10582=FILL_AREA_STYLE ('',( #18402 ) ) ;
#10591=DIRECTION ( 'NONE',  ( -1.000000000000000000, -1.595148023886719315E-16, 0.000000000000000000 ) ) ;
#10597=CARTESIAN_POINT ( 'NONE',  ( -211.5106270998635409, 103.1299228374912360, 29.36128450348865471 ) ) ;
#10602=CARTESIAN_POINT ( 'NONE',  ( 153.4893729001366864, 103.1299228374914492, 29.36128450348865471 ) ) ;
#10614=AXIS2_PLACEMENT_3D ( 'NONE', #7544, #16828, #5995 ) ;
#10617=LINE ( 'NONE', #20083, #759 ) ;
#10630=ORIENTED_EDGE ( 'NONE', *, *, #18406, .F. ) ;
#10632=( NAMED_UNIT ( * ) PLANE_ANGLE_UNIT ( ) SI_UNIT ( $, .RADIAN. ) );
#10636=EDGE_CURVE ( 'NONE', #10482, #3302, #13353, .T. ) ;
#10644=LINE ( 'NONE', #5603, #10002 ) ;
#10651=DIRECTION ( 'NONE',  ( 1.000000000000000000, 5.889072920838430686E-16, -0.000000000000000000 ) ) ;
#10656=COLOUR_RGB ( '', 0.31764706, 0.68627451, 0.89019608) ;
#10662=ORIENTED_EDGE ( 'NONE', *, *, #3857, .F. ) ;
#10667=LINE ( 'NONE', #10465, #20252 ) ;
#10672=CIRCLE ( 'NONE', #9023, 10.00000000000000888 ) ;
#10674=AXIS2_PLACEMENT_3D ( 'NONE', #16223, #18418, #5966 ) ;
#10688=AXIS2_PLACEMENT_3D ( 'NONE', #17827, #17931, #11451 ) ;
#10712=VECTOR ( 'NONE', #12741, 1000.000000000000000 ) ;
#10713=SURFACE_STYLE_FILL_AREA ( #990 ) ;
#10726=VECTOR ( 'NONE', #9082, 1000.000000000000000 ) ;
#10730=DIRECTION ( 'NONE',  ( 1.000000000000000000, -0.000000000000000000, 0.000000000000000000 ) ) ;
#10740=( NAMED_UNIT ( * ) SI_UNIT ( $, .STERADIAN. ) SOLID_ANGLE_UNIT ( ) );
#10747=DIRECTION ( 'NONE',  ( 0.000000000000000000, -1.000000000000000000, 0.000000000000000000 ) ) ;
#10749=FILL_AREA_STYLE ('',( #4566 ) ) ;
#10751=EDGE_CURVE ( 'NONE', #9454, #17589, #19019, .T. ) ;
#10759=VERTEX_POINT ( 'NONE', #8231 ) ;
#10768=ADVANCED_FACE ( 'NONE', ( #11205, #17701, #15989, #4931, #17390 ), #6482, .F. ) ;
#10778=SURFACE_STYLE_USAGE ( .BOTH. , #15425 ) ;
#10788=CARTESIAN_POINT ( 'NONE',  ( 153.4893729001366864, 123.1299228374914634, 170.4174721992565082 ) ) ;
#10789=( LENGTH_UNIT ( ) NAMED_UNIT ( * ) SI_UNIT ( .MILLI., .METRE. ) );
#10792=CIRCLE ( 'NONE', #14736, 10.00000000000000888 ) ;
#10799=SURFACE_STYLE_FILL_AREA ( #2756 ) ;
#10802=CARTESIAN_POINT ( 'NONE',  ( -211.5106270998635409, 103.1299228374912360, 170.4174721992565082 ) ) ;
#10819=VERTEX_POINT ( 'NONE', #11616 ) ;
#10823=SURFACE_STYLE_FILL_AREA ( #4543 ) ;
#10829=FILL_AREA_STYLE ('',( #14118 ) ) ;
#10833=LINE ( 'NONE', #8053, #16884 ) ;
#10834=AXIS2_PLACEMENT_3D ( 'NONE', #9979, #8841, #5451 ) ;
#10836=( GEOMETRIC_REPRESENTATION_CONTEXT ( 3 ) GLOBAL_UNCERTAINTY_ASSIGNED_CONTEXT ( ( #88 ) ) GLOBAL_UNIT_ASSIGNED_CONTEXT ( ( #2098, #2711, #1037 ) ) REPRESENTATION_CONTEXT ( 'NONE', 'WORKASPACE' ) );
#10838=FACE_OUTER_BOUND ( 'NONE', #13883, .T. ) ;
#10856=ORIENTED_EDGE ( 'NONE', *, *, #9072, .F. ) ;
#10867=EDGE_LOOP ( 'NONE', ( #9154, #3474, #16437, #2619 ) ) ;
#10888=( NAMED_UNIT ( * ) SI_UNIT ( $, .STERADIAN. ) SOLID_ANGLE_UNIT ( ) );
#10901=ORIENTED_EDGE ( 'NONE', *, *, #12946, .F. ) ;
#10903=ADVANCED_FACE ( 'NONE', ( #12121, #18393, #4293, #10575, #1679 ), #5126, .F. ) ;
#10927=ORIENTED_EDGE ( 'NONE', *, *, #19777, .F. ) ;
#10937=CARTESIAN_POINT ( 'NONE',  ( 53.48937290013658696, 103.1299228374913923, 170.4174721992565082 ) ) ;
#10942=DIRECTION ( 'NONE',  ( -1.000000000000000000, 0.000000000000000000, -0.000000000000000000 ) ) ;
#10945=( NAMED_UNIT ( * ) PLANE_ANGLE_UNIT ( ) SI_UNIT ( $, .RADIAN. ) );
#10947=VERTEX_POINT ( 'NONE', #9529 ) ;
#10949=CARTESIAN_POINT ( 'NONE',  ( -211.5106270998635409, 113.1299228374912502, 170.4174721992565082 ) ) ;
#10952=FACE_OUTER_BOUND ( 'NONE', #351, .T. ) ;
#10954=ORIENTED_EDGE ( 'NONE', *, *, #14519, .F. ) ;
#10969=ORIENTED_EDGE ( 'NONE', *, *, #16834, .T. ) ;
#10974=DIRECTION ( 'NONE',  ( 0.000000000000000000, 0.000000000000000000, 1.000000000000000000 ) ) ;
#10988=CARTESIAN_POINT ( 'NONE',  ( 53.48937290013658696, 123.1299228374914065, 79.58252780074349175 ) ) ;
#10989=EDGE_CURVE ( 'NONE', #19951, #17875, #858, .T. ) ;
#11000=STYLED_ITEM ( 'NONE', ( #2172 ), #1516 ) ;
#11003=EDGE_LOOP ( 'NONE', ( #2498, #3053, #3315, #18010 ) ) ;
#11007=LINE ( 'NONE', #17178, #13652 ) ;
#11021=VECTOR ( 'NONE', #13521, 1000.000000000000000 ) ;
#11026=( GEOMETRIC_REPRESENTATION_CONTEXT ( 3 ) GLOBAL_UNCERTAINTY_ASSIGNED_CONTEXT ( ( #8588 ) ) GLOBAL_UNIT_ASSIGNED_CONTEXT ( ( #3762, #11896, #2805 ) ) REPRESENTATION_CONTEXT ( 'NONE', 'WORKASPACE' ) );
#11044=DIRECTION ( 'NONE',  ( 0.000000000000000000, -0.000000000000000000, 1.000000000000000000 ) ) ;
#11056=DIRECTION ( 'NONE',  ( 1.000000000000000000, 5.889072920838430686E-16, -0.000000000000000000 ) ) ;
#11060=CARTESIAN_POINT ( 'NONE',  ( 78.48937290013660117, 113.1299228374914208, 29.36128450348865471 ) ) ;
#11062=FACE_BOUND ( 'NONE', #221, .T. ) ;
#11063=FACE_OUTER_BOUND ( 'NONE', #10419, .T. ) ;
#11064=ADVANCED_FACE ( 'NONE', ( #11590 ), #17773, .F. ) ;
#11081=CARTESIAN_POINT ( 'NONE',  ( 78.48937290013660117, 123.1299228374914208, 79.58252780074349175 ) ) ;
#11105=CARTESIAN_POINT ( 'NONE',  ( 78.48937290013661539, 80.91625508013694912, 0.000000000000000000 ) ) ;
#11107=EDGE_LOOP ( 'NONE', ( #3276, #9580, #17335, #1110 ) ) ;
#11110=DIRECTION ( 'NONE',  ( -1.000000000000000000, -0.000000000000000000, -0.000000000000000000 ) ) ;
#11123=ORIENTED_EDGE ( 'NONE', *, *, #6765, .F. ) ;
#11132=SURFACE_SIDE_STYLE ('',( #18848 ) ) ;
#11147=ORIENTED_EDGE ( 'NONE', *, *, #19202, .T. ) ;
#11165=ORIENTED_EDGE ( 'NONE', *, *, #11417, .T. ) ;
#11173=LINE ( 'NONE', #14374, #10712 ) ;
#11176=LINE ( 'NONE', #9432, #19233 ) ;
#11177=EDGE_CURVE ( 'NONE', #5312, #3926, #2210, .T. ) ;
#11182=( LENGTH_UNIT ( ) NAMED_UNIT ( * ) SI_UNIT ( .MILLI., .METRE. ) );
#11194=ORIENTED_EDGE ( 'NONE', *, *, #5234, .F. ) ;
#11205=FACE_BOUND ( 'NONE', #1183, .T. ) ;
#11206=DIRECTION ( 'NONE',  ( 1.000000000000000000, 5.889072920838430686E-16, -0.000000000000000000 ) ) ;
#11219=VERTEX_POINT ( 'NONE', #14453 ) ;
#11220=MECHANICAL_DESIGN_GEOMETRIC_PRESENTATION_REPRESENTATION('',(#4981),#2994);
#11221=ORIENTED_EDGE ( 'NONE', *, *, #14062, .F. ) ;
#11239=ORIENTED_EDGE ( 'NONE', *, *, #1076, .T. ) ;
#11250=DIRECTION ( 'NONE',  ( 0.000000000000000000, 1.000000000000000000, 0.000000000000000000 ) ) ;
#11256=FACE_OUTER_BOUND ( 'NONE', #17018, .T. ) ;
#11270=DIRECTION ( 'NONE',  ( 0.000000000000000000, 1.000000000000000000, 0.000000000000000000 ) ) ;
#11275=ORIENTED_EDGE ( 'NONE', *, *, #20106, .F. ) ;
#11278=CIRCLE ( 'NONE', #12281, 10.00000000000000888 ) ;
#11284=FACE_OUTER_BOUND ( 'NONE', #20241, .T. ) ;
#11287=( LENGTH_UNIT ( ) NAMED_UNIT ( * ) SI_UNIT ( .MILLI., .METRE. ) );
#11288=EDGE_CURVE ( 'NONE', #19445, #3672, #10792, .T. ) ;
#11290=CLOSED_SHELL ( 'NONE', ( #11553, #2924, #8037, #8494, #5371, #16856, #4833, #6282, #5498, #10198, #11064, #2347, #15737, #20070, #15200, #13447, #6121, #19788, #11409, #17650 ) ) ;
#11301=DIRECTION ( 'NONE',  ( 1.000000000000000000, 5.889072920838430686E-16, -0.000000000000000000 ) ) ;
#11307=PRESENTATION_STYLE_ASSIGNMENT (( #1825 ) ) ;
#11313=CARTESIAN_POINT ( 'NONE',  ( 53.48937290013658696, 113.1299228374914065, 29.36128450348865471 ) ) ;
#11319=ORIENTED_EDGE ( 'NONE', *, *, #8122, .F. ) ;
#11331=LINE ( 'NONE', #8760, #17570 ) ;
#11338=CARTESIAN_POINT ( 'NONE',  ( 133.4893729001365443, 113.1299228374914634, 170.4174721992565082 ) ) ;
#11364=SURFACE_STYLE_USAGE ( .BOTH. , #9920 ) ;
#11367=SURFACE_SIDE_STYLE ('',( #328 ) ) ;
#11368=DIRECTION ( 'NONE',  ( 0.000000000000000000, 1.000000000000000000, 0.000000000000000000 ) ) ;
#11372=CARTESIAN_POINT ( 'NONE',  ( -0.000000000000000000, 167.9162550801369491, 250.0000000000000000 ) ) ;
#11374=SURFACE_STYLE_FILL_AREA ( #6759 ) ;
#11378=EDGE_CURVE ( 'NONE', #1858, #12290, #14552, .T. ) ;
#11379=EDGE_LOOP ( 'NONE', ( #13296, #10563, #2306, #16835 ) ) ;
#11386=CARTESIAN_POINT ( 'NONE',  ( 78.48937290013660117, 103.1299228374914065, 29.36128450348865471 ) ) ;
#11387=FILL_AREA_STYLE ('',( #912 ) ) ;
#11393=ADVANCED_FACE ( 'NONE', ( #14978 ), #541, .F. ) ;
#11395=DIRECTION ( 'NONE',  ( 1.000000000000000000, 5.889072920838430686E-16, -0.000000000000000000 ) ) ;
#11396=DIRECTION ( 'NONE',  ( 5.889072920838430686E-16, -1.000000000000000000, 0.000000000000000000 ) ) ;
#11409=ADVANCED_FACE ( 'NONE', ( #5495 ), #6946, .F. ) ;
#11412=PRODUCT ( 'Part10^Assem2', 'Part10^Assem2', '', ( #18285 ) ) ;
#11413=ORIENTED_EDGE ( 'NONE', *, *, #14830, .F. ) ;
#11417=EDGE_CURVE ( 'NONE', #5899, #6147, #5291, .T. ) ;
#11421=ORIENTED_EDGE ( 'NONE', *, *, #3084, .T. ) ;
#11422=AXIS2_PLACEMENT_3D ( 'NONE', #2215, #10162, #16467 ) ;
#11424=CARTESIAN_POINT ( 'NONE',  ( 53.48937290013659407, 167.9162550801369491, 250.0000000000000000 ) ) ;
#11427=CYLINDRICAL_SURFACE ( 'NONE', #402, 10.00000000000000888 ) ;
#11436=VERTEX_POINT ( 'NONE', #6754 ) ;
#11451=DIRECTION ( 'NONE',  ( 0.000000000000000000, 1.000000000000000000, 0.000000000000000000 ) ) ;
#11460=FACE_OUTER_BOUND ( 'NONE', #2992, .T. ) ;
#11466=FILL_AREA_STYLE_COLOUR ( '', #15332 ) ;
#11467=SURFACE_STYLE_USAGE ( .BOTH. , #3641 ) ;
#11497=MECHANICAL_DESIGN_GEOMETRIC_PRESENTATION_REPRESENTATION('',(#2296),#18100);
#11522=EDGE_CURVE ( 'NONE', #10759, #4977, #9620, .T. ) ;
#11526=FILL_AREA_STYLE ('',( #14621 ) ) ;
#11528=VECTOR ( 'NONE', #6266, 1000.000000000000000 ) ;
#11532=EDGE_CURVE ( 'NONE', #17418, #18122, #12261, .T. ) ;
#11553=ADVANCED_FACE ( 'NONE', ( #4251 ), #1013, .F. ) ;
#11559=( NAMED_UNIT ( * ) PLANE_ANGLE_UNIT ( ) SI_UNIT ( $, .RADIAN. ) );
#11569=CARTESIAN_POINT ( 'NONE',  ( 153.4893729001366864, 113.1299228374914634, 29.36128450348865471 ) ) ;
#11590=FACE_OUTER_BOUND ( 'NONE', #17571, .T. ) ;
#11593=SURFACE_STYLE_USAGE ( .BOTH. , #5320 ) ;
#11596=AXIS2_PLACEMENT_3D ( 'NONE', #10389, #8745, #2745 ) ;
#11605=ORIENTED_EDGE ( 'NONE', *, *, #11522, .T. ) ;
#11616=CARTESIAN_POINT ( 'NONE',  ( 153.4893729001366864, 103.1299228374914492, 170.4174721992565082 ) ) ;
#11622=CARTESIAN_POINT ( 'NONE',  ( 153.4893729001366580, 145.9162550801369491, 0.000000000000000000 ) ) ;
#11623=EDGE_LOOP ( 'NONE', ( #7785, #20155 ) ) ;
#11626=AXIS2_PLACEMENT_3D ( 'NONE', #2465, #13766, #18494 ) ;
#11635=VECTOR ( 'NONE', #5876, 1000.000000000000000 ) ;
#11638=LINE ( 'NONE', #5465, #3301 ) ;
#11640=( GEOMETRIC_REPRESENTATION_CONTEXT ( 3 ) GLOBAL_UNCERTAINTY_ASSIGNED_CONTEXT ( ( #10119 ) ) GLOBAL_UNIT_ASSIGNED_CONTEXT ( ( #19963, #16501, #5874 ) ) REPRESENTATION_CONTEXT ( 'NONE', 'WORKASPACE' ) );
#11642=CARTESIAN_POINT ( 'NONE',  ( 149.0892156028631348, 80.91625508013694912, 250.0000000000000000 ) ) ;
#11647=SURFACE_SIDE_STYLE ('',( #17504 ) ) ;
#11649=EDGE_CURVE ( 'NONE', #6545, #16028, #10833, .T. ) ;
#11651=STYLED_ITEM ( 'NONE', ( #8898 ), #1321 ) ;
#11652=STYLED_ITEM ( 'NONE', ( #14375 ), #192 ) ;
#11661=VERTEX_POINT ( 'NONE', #6416 ) ;
#11665=FILL_AREA_STYLE ('',( #3634 ) ) ;
#11695=VECTOR ( 'NONE', #2197, 1000.000000000000000 ) ;
#11701=CARTESIAN_POINT ( 'NONE',  ( 98.48937290013660117, 80.91625508013694912, 0.000000000000000000 ) ) ;
#11705=UNCERTAINTY_MEASURE_WITH_UNIT (LENGTH_MEASURE( 1.000000000000000082E-05 ), #2654, 'distance_accuracy_value', 'NONE');
#11708=FILL_AREA_STYLE_COLOUR ( '', #5569 ) ;
#11714=DIRECTION ( 'NONE',  ( 1.000000000000000000, 0.000000000000000000, 0.000000000000000000 ) ) ;
#11725=VERTEX_POINT ( 'NONE', #14742 ) ;
#11741=( NAMED_UNIT ( * ) PLANE_ANGLE_UNIT ( ) SI_UNIT ( $, .RADIAN. ) );
#11742=ORIENTED_EDGE ( 'NONE', *, *, #7710, .F. ) ;
#11752=CARTESIAN_POINT ( 'NONE',  ( 53.48937290013658696, 113.1299228374914065, 79.58252780074349175 ) ) ;
#11763=CARTESIAN_POINT ( 'NONE',  ( 78.48937290013660117, 113.1299228374914208, 170.4174721992565082 ) ) ;
#11765=ORIENTED_EDGE ( 'NONE', *, *, #370, .T. ) ;
#11772=DIRECTION ( 'NONE',  ( -1.000000000000000000, 0.000000000000000000, 0.000000000000000000 ) ) ;
#11774=SURFACE_SIDE_STYLE ('',( #16732 ) ) ;
#11781=CARTESIAN_POINT ( 'NONE',  ( 82.88953019741013861, 80.91625508013694912, 245.0000000000000000 ) ) ;
#11789=CARTESIAN_POINT ( 'NONE',  ( 0.000000000000000000, 167.9162550801369491, -97.94896630388704750 ) ) ;
#11791=CIRCLE ( 'NONE', #18343, 10.00000000000000888 ) ;
#11796=( NAMED_UNIT ( * ) SI_UNIT ( $, .STERADIAN. ) SOLID_ANGLE_UNIT ( ) );
#11800=FILL_AREA_STYLE ('',( #19908 ) ) ;
#11804=LINE ( 'NONE', #14882, #11695 ) ;
#11807=ORIENTED_EDGE ( 'NONE', *, *, #14260, .T. ) ;
#11811=SURFACE_STYLE_FILL_AREA ( #1147 ) ;
#11813=VERTEX_POINT ( 'NONE', #10602 ) ;
#11815=MECHANICAL_DESIGN_GEOMETRIC_PRESENTATION_REPRESENTATION('',(#9165),#9837);
#11821=LINE ( 'NONE', #17036, #3009 ) ;
#11832=DIRECTION ( 'NONE',  ( 1.000000000000000000, 5.889072920838430686E-16, -0.000000000000000000 ) ) ;
#11841=EDGE_LOOP ( 'NONE', ( #12028, #12144 ) ) ;
#11872=CARTESIAN_POINT ( 'NONE',  ( 149.0892156028631348, 167.9162550801369491, 250.0000000000000000 ) ) ;
#11873=AXIS2_PLACEMENT_3D ( 'NONE', #16822, #1005, #4246 ) ;
#11874=CARTESIAN_POINT ( 'NONE',  ( 98.48937290013662960, 123.1299228374914350, 220.6387154965113382 ) ) ;
#11881=CARTESIAN_POINT ( 'NONE',  ( 153.4893729001366864, 113.1299228374914634, 220.6387154965113382 ) ) ;
#11884=ORIENTED_EDGE ( 'NONE', *, *, #4238, .T. ) ;
#11896=( NAMED_UNIT ( * ) PLANE_ANGLE_UNIT ( ) SI_UNIT ( $, .RADIAN. ) );
#11900=SURFACE_STYLE_USAGE ( .BOTH. , #938 ) ;
#11910=DIRECTION ( 'NONE',  ( 0.000000000000000000, -0.000000000000000000, -1.000000000000000000 ) ) ;
#11916=ORIENTED_EDGE ( 'NONE', *, *, #10989, .F. ) ;
#11917=ADVANCED_FACE ( 'NONE', ( #7315, #12071, #12854, #461, #11284 ), #17009, .F. ) ;
#11933=FILL_AREA_STYLE ('',( #2542 ) ) ;
#11937=ORIENTED_EDGE ( 'NONE', *, *, #12395, .F. ) ;
#11945=VECTOR ( 'NONE', #16360, 1000.000000000000000 ) ;
#11951=MECHANICAL_DESIGN_GEOMETRIC_PRESENTATION_REPRESENTATION('',(#14232),#18836);
#11952=AXIS2_PLACEMENT_3D ( 'NONE', #10530, #7341, #18661 ) ;
#11956=CARTESIAN_POINT ( 'NONE',  ( 0.000000000000000000, 34.32473510485366575, 0.000000000000000000 ) ) ;
#11968=ORIENTED_EDGE ( 'NONE', *, *, #805, .F. ) ;
#11969=MECHANICAL_DESIGN_GEOMETRIC_PRESENTATION_REPRESENTATION('',(#4065),#747);
#11970=COLOUR_RGB ( '', 0.31764706, 0.68627451, 0.89019608) ;
#11975=APPLICATION_CONTEXT ( 'automotive_design' ) ;
#11979=AXIS2_PLACEMENT_3D ( 'NONE', #6553, #3249, #18699 ) ;
#11987=SURFACE_SIDE_STYLE ('',( #5901 ) ) ;
#11988=CARTESIAN_POINT ( 'NONE',  ( 153.4893729001366580, 0.000000000000000000, 0.000000000000000000 ) ) ;
#11989=MECHANICAL_DESIGN_GEOMETRIC_PRESENTATION_REPRESENTATION('',(#5412),#9017);
#12006=DIRECTION ( 'NONE',  ( 1.000000000000000000, 5.889072920838430686E-16, -0.000000000000000000 ) ) ;
#12022=CYLINDRICAL_SURFACE ( 'NONE', #2360, 10.00000000000000888 ) ;
#12028=ORIENTED_EDGE ( 'NONE', *, *, #3518, .F. ) ;
#12036=ORIENTED_EDGE ( 'NONE', *, *, #9186, .T. ) ;
#12039=FILL_AREA_STYLE_COLOUR ( '', #5671 ) ;
#12055=EDGE_CURVE ( 'NONE', #5899, #3093, #18164, .T. ) ;
#12058=VERTEX_POINT ( 'NONE', #13374 ) ;
#12060=EDGE_CURVE ( 'NONE', #825, #6147, #14561, .T. ) ;
#12067=DIRECTION ( 'NONE',  ( 0.000000000000000000, 1.000000000000000000, 0.000000000000000000 ) ) ;
#12068=DIRECTION ( 'NONE',  ( 1.000000000000000000, 5.889072920838430686E-16, -0.000000000000000000 ) ) ;
#12071=FACE_BOUND ( 'NONE', #600, .T. ) ;
#12073=EDGE_CURVE ( 'NONE', #7788, #345, #400, .T. ) ;
#12077=ORIENTED_EDGE ( 'NONE', *, *, #7208, .T. ) ;
#12078=ORIENTED_EDGE ( 'NONE', *, *, #19600, .F. ) ;
#12080=EDGE_CURVE ( 'NONE', #6194, #10819, #1159, .T. ) ;
#12082=DIRECTION ( 'NONE',  ( 0.000000000000000000, 1.000000000000000000, 0.000000000000000000 ) ) ;
#12083=( NAMED_UNIT ( * ) SI_UNIT ( $, .STERADIAN. ) SOLID_ANGLE_UNIT ( ) );
#12092=DIRECTION ( 'NONE',  ( 0.000000000000000000, -0.000000000000000000, -1.000000000000000000 ) ) ;
#12098=FACE_OUTER_BOUND ( 'NONE', #10867, .T. ) ;
#12100=SURFACE_STYLE_FILL_AREA ( #11800 ) ;
#12101=STYLED_ITEM ( 'NONE', ( #16340 ), #11393 ) ;
#12103=CIRCLE ( 'NONE', #898, 10.00000000000000888 ) ;
#12105=FACE_OUTER_BOUND ( 'NONE', #17585, .T. ) ;
#12112=ORIENTED_EDGE ( 'NONE', *, *, #5348, .T. ) ;
#12121=FACE_BOUND ( 'NONE', #2857, .T. ) ;
#12124=ADVANCED_FACE ( 'NONE', ( #5967 ), #8854, .F. ) ;
#12129=CARTESIAN_POINT ( 'NONE',  ( 0.000000000000000000, 145.9162550801369491, -97.94896630388704750 ) ) ;
#12137=FACE_BOUND ( 'NONE', #12641, .T. ) ;
#12144=ORIENTED_EDGE ( 'NONE', *, *, #1906, .F. ) ;
#12159=MECHANICAL_DESIGN_GEOMETRIC_PRESENTATION_REPRESENTATION('',(#10169),#5568);
#12164=EDGE_LOOP ( 'NONE', ( #1334, #8347, #11807, #6914 ) ) ;
#12180=VECTOR ( 'NONE', #9746, 1000.000000000000000 ) ;
#12182=ORIENTED_EDGE ( 'NONE', *, *, #15982, .F. ) ;
#12186=SURFACE_STYLE_USAGE ( .BOTH. , #2701 ) ;
#12191=AXIS2_PLACEMENT_3D ( 'NONE', #10949, #320, #16027 ) ;
#12196=CARTESIAN_POINT ( 'NONE',  ( 178.4893729001365443, 0.000000000000000000, -97.94896630388704750 ) ) ;
#12198=DIRECTION ( 'NONE',  ( 0.000000000000000000, -1.000000000000000000, 0.000000000000000000 ) ) ;
#12221=CARTESIAN_POINT ( 'NONE',  ( 133.4893729001365728, 0.000000000000000000, 0.000000000000000000 ) ) ;
#12233=DIRECTION ( 'NONE',  ( -1.000000000000000000, -2.135044278125301096E-16, 0.000000000000000000 ) ) ;
#12237=( NAMED_UNIT ( * ) SI_UNIT ( $, .STERADIAN. ) SOLID_ANGLE_UNIT ( ) );
#12240=EDGE_LOOP ( 'NONE', ( #8468, #14774, #15058, #7712 ) ) ;
#12258=ORIENTED_EDGE ( 'NONE', *, *, #8489, .T. ) ;
#12259=AXIS2_PLACEMENT_3D ( 'NONE', #7686, #7990, #20255 ) ;
#12261=CIRCLE ( 'NONE', #15581, 10.00000000000000888 ) ;
#12264=EDGE_CURVE ( 'NONE', #17965, #18122, #3385, .T. ) ;
#12266=CARTESIAN_POINT ( 'NONE',  ( 0.000000000000000000, 80.91625508013694912, 250.0000000000000000 ) ) ;
#12271=VECTOR ( 'NONE', #12006, 1000.000000000000000 ) ;
#12272=CARTESIAN_POINT ( 'NONE',  ( 178.4893729001365728, 113.1299228374914918, 29.36128450348865471 ) ) ;
#12281=AXIS2_PLACEMENT_3D ( 'NONE', #17218, #105, #18553 ) ;
#12286=MECHANICAL_DESIGN_GEOMETRIC_PRESENTATION_REPRESENTATION('',(#10004),#6726);
#12289=DIRECTION ( 'NONE',  ( 0.000000000000000000, 0.000000000000000000, -1.000000000000000000 ) ) ;
#12290=VERTEX_POINT ( 'NONE', #11424 ) ;
#12294=MECHANICAL_DESIGN_GEOMETRIC_PRESENTATION_REPRESENTATION('',(#4066),#18206);
#12302=MECHANICAL_DESIGN_GEOMETRIC_PRESENTATION_REPRESENTATION('',(#15285),#16615);
#12307=VECTOR ( 'NONE', #5309, 1000.000000000000000 ) ;
#12319=ORIENTED_EDGE ( 'NONE', *, *, #4583, .F. ) ;
#12330=CARTESIAN_POINT ( 'NONE',  ( 153.4893729001366864, 113.1299228374914634, 220.6387154965113382 ) ) ;
#12340=SURFACE_SIDE_STYLE ('',( #7699 ) ) ;
#12351=FACE_OUTER_BOUND ( 'NONE', #9212, .T. ) ;
#12359=DIRECTION ( 'NONE',  ( 0.000000000000000000, 1.000000000000000000, 0.000000000000000000 ) ) ;
#12380=FACE_OUTER_BOUND ( 'NONE', #8847, .T. ) ;
#12384=PRESENTATION_STYLE_ASSIGNMENT (( #20085 ) ) ;
#12389=CARTESIAN_POINT ( 'NONE',  ( 178.4893729001365728, 103.1299228374914776, 170.4174721992565082 ) ) ;
#12395=EDGE_CURVE ( 'NONE', #10424, #7147, #2738, .T. ) ;
#12404=CARTESIAN_POINT ( 'NONE',  ( 78.48937290013660117, 145.9162550801369491, 250.0000000000000000 ) ) ;
#12421=EDGE_LOOP ( 'NONE', ( #18926, #13226 ) ) ;
#12443=FACE_OUTER_BOUND ( 'NONE', #3676, .T. ) ;
#12449=ORIENTED_EDGE ( 'NONE', *, *, #18592, .F. ) ;
#12452=FACE_BOUND ( 'NONE', #15500, .T. ) ;
#12453=VERTEX_POINT ( 'NONE', #20031 ) ;
#12484=AXIS2_PLACEMENT_3D ( 'NONE', #1114, #18131, #4035 ) ;
#12493=AXIS2_PLACEMENT_3D ( 'NONE', #3285, #9562, #15878 ) ;
#12495=AXIS2_PLACEMENT_3D ( 'NONE', #12129, #2942, #1174 ) ;
#12508=DIRECTION ( 'NONE',  ( 1.000000000000000000, 0.000000000000000000, 0.000000000000000000 ) ) ;
#12531=SURFACE_STYLE_FILL_AREA ( #15748 ) ;
#12541=VECTOR ( 'NONE', #12608, 1000.000000000000000 ) ;
#12542=COLOUR_RGB ( '', 0.40784314, 0.44705882, 0.49803922) ;
#12558=CARTESIAN_POINT ( 'NONE',  ( 53.48937290013659407, 145.9162550801369491, 250.0000000000000000 ) ) ;
#12577=LINE ( 'NONE', #12794, #19764 ) ;
#12594=EDGE_CURVE ( 'NONE', #16393, #11219, #15633, .T. ) ;
#12600=DIRECTION ( 'NONE',  ( -0.000000000000000000, -0.000000000000000000, 1.000000000000000000 ) ) ;
#12602=AXIS2_PLACEMENT_3D ( 'NONE', #12272, #20091, #20300 ) ;
#12608=DIRECTION ( 'NONE',  ( 1.000000000000000000, 5.889072920838430686E-16, -0.000000000000000000 ) ) ;
#12624=VECTOR ( 'NONE', #15592, 1000.000000000000000 ) ;
#12626=AXIS2_PLACEMENT_3D ( 'NONE', #2204, #19506, #11714 ) ;
#12627=SURFACE_STYLE_USAGE ( .BOTH. , #15450 ) ;
#12629=LINE ( 'NONE', #4590, #14986 ) ;
#12633=( LENGTH_UNIT ( ) NAMED_UNIT ( * ) SI_UNIT ( .MILLI., .METRE. ) );
#12636=( LENGTH_UNIT ( ) NAMED_UNIT ( * ) SI_UNIT ( .MILLI., .METRE. ) );
#12641=EDGE_LOOP ( 'NONE', ( #18511, #13258 ) ) ;
#12642=CARTESIAN_POINT ( 'NONE',  ( 143.0892156028631348, 167.9162550801369491, 245.0000000000000000 ) ) ;
#12653=CARTESIAN_POINT ( 'NONE',  ( 0.000000000000000000, 80.91625508013694912, 250.0000000000000000 ) ) ;
#12655=( GEOMETRIC_REPRESENTATION_CONTEXT ( 3 ) GLOBAL_UNCERTAINTY_ASSIGNED_CONTEXT ( ( #18154 ) ) GLOBAL_UNIT_ASSIGNED_CONTEXT ( ( #17747, #13132, #5289 ) ) REPRESENTATION_CONTEXT ( 'NONE', 'WORKASPACE' ) );
#12668=FILL_AREA_STYLE_COLOUR ( '', #15661 ) ;
#12695=DIRECTION ( 'NONE',  ( -0.000000000000000000, -0.000000000000000000, 1.000000000000000000 ) ) ;
#12696=( NAMED_UNIT ( * ) SI_UNIT ( $, .STERADIAN. ) SOLID_ANGLE_UNIT ( ) );
#12709=EDGE_CURVE ( 'NONE', #17965, #12453, #7081, .T. ) ;
#12713=FILL_AREA_STYLE ('',( #9587 ) ) ;
#12719=PRESENTATION_STYLE_ASSIGNMENT (( #4664 ) ) ;
#12731=AXIS2_PLACEMENT_3D ( 'NONE', #2558, #15362, #13596 ) ;
#12741=DIRECTION ( 'NONE',  ( 0.000000000000000000, 0.000000000000000000, 1.000000000000000000 ) ) ;
#12753=SURFACE_STYLE_USAGE ( .BOTH. , #17463 ) ;
#12774=CARTESIAN_POINT ( 'NONE',  ( -211.5106270998635409, 103.1299228374912360, 220.6387154965113382 ) ) ;
#12777=CARTESIAN_POINT ( 'NONE',  ( 98.48937290013660117, 167.9162550801369491, 250.0000000000000000 ) ) ;
#12780=CIRCLE ( 'NONE', #5859, 10.00000000000000888 ) ;
#12794=CARTESIAN_POINT ( 'NONE',  ( 78.48937290013660117, 145.9162550801369491, -140.0000000000001137 ) ) ;
#12809=EDGE_CURVE ( 'NONE', #10759, #2483, #18777, .T. ) ;
#12820=DIRECTION ( 'NONE',  ( 0.000000000000000000, 1.000000000000000000, 0.000000000000000000 ) ) ;
#12822=CARTESIAN_POINT ( 'NONE',  ( 178.4893729001365443, 167.9162550801369491, 250.0000000000000000 ) ) ;
#12838=SURFACE_STYLE_USAGE ( .BOTH. , #5001 ) ;
#12841=SURFACE_STYLE_FILL_AREA ( #15837 ) ;
#12842=ORIENTED_EDGE ( 'NONE', *, *, #7506, .F. ) ;
#12844=LINE ( 'NONE', #3468, #12180 ) ;
#12846=( NAMED_UNIT ( * ) SI_UNIT ( $, .STERADIAN. ) SOLID_ANGLE_UNIT ( ) );
#12854=FACE_BOUND ( 'NONE', #3485, .T. ) ;
#12864=AXIS2_PLACEMENT_3D ( 'NONE', #13864, #6044, #4498 ) ;
#12866=COLOUR_RGB ( '', 0.08235294, 0.09019608, 0.10196078) ;
#12883=DIRECTION ( 'NONE',  ( 0.000000000000000000, 1.000000000000000000, 0.000000000000000000 ) ) ;
#12893=COLOUR_RGB ( '', 0.40784314, 0.44705882, 0.49803922) ;
#12899=DIRECTION ( 'NONE',  ( -0.000000000000000000, -0.000000000000000000, 1.000000000000000000 ) ) ;
#12914=ORIENTED_EDGE ( 'NONE', *, *, #18188, .F. ) ;
#12925=ADVANCED_FACE ( 'NONE', ( #3643 ), #9926, .F. ) ;
#12929=CARTESIAN_POINT ( 'NONE',  ( -211.5106270998635409, 103.1299228374912360, 29.36128450348865471 ) ) ;
#12932=ORIENTED_EDGE ( 'NONE', *, *, #6342, .T. ) ;
#12935=( NAMED_UNIT ( * ) PLANE_ANGLE_UNIT ( ) SI_UNIT ( $, .RADIAN. ) );
#12945=ORIENTED_EDGE ( 'NONE', *, *, #4108, .F. ) ;
#12946=EDGE_CURVE ( 'NONE', #14468, #16599, #14671, .T. ) ;
#12962=CARTESIAN_POINT ( 'NONE',  ( 78.48937290013660117, 103.1299228374914065, 220.6387154965113382 ) ) ;
#12980=CARTESIAN_POINT ( 'NONE',  ( 143.0892156028631348, 167.9162550801369491, 245.0000000000000000 ) ) ;
#12988=CARTESIAN_POINT ( 'NONE',  ( 0.000000000000000000, 0.000000000000000000, 245.0000000000000000 ) ) ;
#12992=DIRECTION ( 'NONE',  ( 1.000000000000000000, 9.815121534730717399E-17, -0.000000000000000000 ) ) ;
#12997=AXIS2_PLACEMENT_3D ( 'NONE', #19551, #15041, #18106 ) ;
#13001=ORIENTED_EDGE ( 'NONE', *, *, #1540, .T. ) ;
#13013=AXIS2_PLACEMENT_3D ( 'NONE', #9355, #4716, #14191 ) ;
#13029=( GEOMETRIC_REPRESENTATION_CONTEXT ( 3 ) GLOBAL_UNCERTAINTY_ASSIGNED_CONTEXT ( ( #5513 ) ) GLOBAL_UNIT_ASSIGNED_CONTEXT ( ( #3497, #17483, #7916 ) ) REPRESENTATION_CONTEXT ( 'NONE', 'WORKASPACE' ) );
#13030=PRESENTATION_STYLE_ASSIGNMENT (( #19468 ) ) ;
#13031=ORIENTED_EDGE ( 'NONE', *, *, #18406, .T. ) ;
#13035=UNCERTAINTY_MEASURE_WITH_UNIT (LENGTH_MEASURE( 1.000000000000000082E-05 ), #11182, 'distance_accuracy_value', 'NONE');
#13039=SURFACE_STYLE_FILL_AREA ( #5086 ) ;
#13048=( LENGTH_UNIT ( ) NAMED_UNIT ( * ) SI_UNIT ( .MILLI., .METRE. ) );
#13054=EDGE_LOOP ( 'NONE', ( #1200, #1750 ) ) ;
#13076=ORIENTED_EDGE ( 'NONE', *, *, #7506, .T. ) ;
#13081=ORIENTED_EDGE ( 'NONE', *, *, #9585, .F. ) ;
#13088=ORIENTED_EDGE ( 'NONE', *, *, #18707, .T. ) ;
#13095=LINE ( 'NONE', #17600, #9206 ) ;
#13129=DIRECTION ( 'NONE',  ( 1.000000000000000000, 0.000000000000000000, 0.000000000000000000 ) ) ;
#13132=( NAMED_UNIT ( * ) PLANE_ANGLE_UNIT ( ) SI_UNIT ( $, .RADIAN. ) );
#13141=LINE ( 'NONE', #16532, #17905 ) ;
#13150=PLANE ( 'NONE',  #19852 ) ;
#13159=PLANE ( 'NONE',  #15770 ) ;
#13164=AXIS2_PLACEMENT_3D ( 'NONE', #1314, #20305, #19138 ) ;
#13172=ORIENTED_EDGE ( 'NONE', *, *, #4583, .T. ) ;
#13179=DIRECTION ( 'NONE',  ( 0.000000000000000000, -1.000000000000000000, 0.000000000000000000 ) ) ;
#13198=MECHANICAL_DESIGN_GEOMETRIC_PRESENTATION_REPRESENTATION('',(#13818),#7570);
#13210=CARTESIAN_POINT ( 'NONE',  ( 149.0892156028631348, 80.91625508013694912, 245.0000000000000000 ) ) ;
#13220=UNCERTAINTY_MEASURE_WITH_UNIT (LENGTH_MEASURE( 1.000000000000000082E-05 ), #5455, 'distance_accuracy_value', 'NONE');
#13224=UNCERTAINTY_MEASURE_WITH_UNIT (LENGTH_MEASURE( 1.000000000000000082E-05 ), #19279, 'distance_accuracy_value', 'NONE');
#13226=ORIENTED_EDGE ( 'NONE', *, *, #15906, .T. ) ;
#13231=DIRECTION ( 'NONE',  ( 0.000000000000000000, 0.000000000000000000, 1.000000000000000000 ) ) ;
#13239=EDGE_LOOP ( 'NONE', ( #8436, #17853 ) ) ;
#13244=EDGE_LOOP ( 'NONE', ( #11275, #7090, #10969, #9357 ) ) ;
#13245=DIRECTION ( 'NONE',  ( 0.000000000000000000, 0.000000000000000000, 1.000000000000000000 ) ) ;
#13249=SURFACE_SIDE_STYLE ('',( #16260 ) ) ;
#13253=DIRECTION ( 'NONE',  ( 1.000000000000000000, -0.000000000000000000, 0.000000000000000000 ) ) ;
#13258=ORIENTED_EDGE ( 'NONE', *, *, #9804, .T. ) ;
#13289=UNCERTAINTY_MEASURE_WITH_UNIT (LENGTH_MEASURE( 1.000000000000000082E-05 ), #10789, 'distance_accuracy_value', 'NONE');
#13293=COLOUR_RGB ( '', 0.72549020, 0.75294118, 0.79215686) ;
#13296=ORIENTED_EDGE ( 'NONE', *, *, #7208, .F. ) ;
#13306=AXIS2_PLACEMENT_3D ( 'NONE', #3258, #164, #14081 ) ;
#13323=ORIENTED_EDGE ( 'NONE', *, *, #8790, .T. ) ;
#13326=ORIENTED_EDGE ( 'NONE', *, *, #150, .F. ) ;
#13330=CYLINDRICAL_SURFACE ( 'NONE', #9251, 10.00000000000000888 ) ;
#13332=SURFACE_SIDE_STYLE ('',( #7235 ) ) ;
#13341=CYLINDRICAL_SURFACE ( 'NONE', #5786, 10.00000000000000888 ) ;
#13342=CARTESIAN_POINT ( 'NONE',  ( -211.5106270998635409, 113.1299228374912502, 29.36128450348865471 ) ) ;
#13348=DIRECTION ( 'NONE',  ( 1.000000000000000000, 5.889072920838430686E-16, -0.000000000000000000 ) ) ;
#13350=CIRCLE ( 'NONE', #149, 10.00000000000000888 ) ;
#13353=CIRCLE ( 'NONE', #10372, 10.00000000000000888 ) ;
#13364=DIRECTION ( 'NONE',  ( 9.815121534730717399E-17, -1.000000000000000000, 0.000000000000000000 ) ) ;
#13366=UNCERTAINTY_MEASURE_WITH_UNIT (LENGTH_MEASURE( 1.000000000000000082E-05 ), #3122, 'distance_accuracy_value', 'NONE');
#13374=CARTESIAN_POINT ( 'NONE',  ( 133.4893729001365728, 80.91625508013694912, 0.000000000000000000 ) ) ;
#13376=SURFACE_SIDE_STYLE ('',( #5223 ) ) ;
#13433=CYLINDRICAL_SURFACE ( 'NONE', #12484, 10.00000000000000888 ) ;
#13435=PRESENTATION_STYLE_ASSIGNMENT (( #7045 ) ) ;
#13442=VERTEX_POINT ( 'NONE', #590 ) ;
#13444=COLOUR_RGB ( '', 0.08235294, 0.09019608, 0.10196078) ;
#13447=ADVANCED_FACE ( 'NONE', ( #5159 ), #11427, .F. ) ;
#13452=SURFACE_STYLE_FILL_AREA ( #555 ) ;
#13457=FILL_AREA_STYLE_COLOUR ( '', #14271 ) ;
#13458=CYLINDRICAL_SURFACE ( 'NONE', #7027, 10.00000000000000888 ) ;
#13460=DIRECTION ( 'NONE',  ( 1.000000000000000000, 5.889072920838430686E-16, -0.000000000000000000 ) ) ;
#13465=ORIENTED_EDGE ( 'NONE', *, *, #10485, .T. ) ;
#13469=ORIENTED_EDGE ( 'NONE', *, *, #3219, .T. ) ;
#13470=AXIS2_PLACEMENT_3D ( 'NONE', #17854, #5295, #636 ) ;
#13479=LINE ( 'NONE', #1062, #7324 ) ;
#13491=VECTOR ( 'NONE', #4398, 1000.000000000000000 ) ;
#13495=ORIENTED_EDGE ( 'NONE', *, *, #8362, .T. ) ;
#13498=DIRECTION ( 'NONE',  ( 0.000000000000000000, 1.000000000000000000, 0.000000000000000000 ) ) ;
#13502=FILL_AREA_STYLE_COLOUR ( '', #17977 ) ;
#13510=ADVANCED_FACE ( 'NONE', ( #8840 ), #5753, .F. ) ;
#13521=DIRECTION ( 'NONE',  ( -1.000000000000000000, -0.000000000000000000, -0.000000000000000000 ) ) ;
#13539=ORIENTED_EDGE ( 'NONE', *, *, #150, .T. ) ;
#13547=EDGE_CURVE ( 'NONE', #6655, #4371, #419, .T. ) ;
#13552=( LENGTH_UNIT ( ) NAMED_UNIT ( * ) SI_UNIT ( .MILLI., .METRE. ) );
#13563=EDGE_LOOP ( 'NONE', ( #14696, #2802 ) ) ;
#13564=CARTESIAN_POINT ( 'NONE',  ( 53.48937290013659407, 145.9162550801369491, 250.0000000000000000 ) ) ;
#13566=ORIENTED_EDGE ( 'NONE', *, *, #14982, .T. ) ;
#13587=VERTEX_POINT ( 'NONE', #10788 ) ;
#13596=DIRECTION ( 'NONE',  ( 0.000000000000000000, 0.000000000000000000, 1.000000000000000000 ) ) ;
#13598=CIRCLE ( 'NONE', #4710, 10.00000000000000888 ) ;
#13609=EDGE_LOOP ( 'NONE', ( #4794, #2256, #364, #19054 ) ) ;
#13611=COLOUR_RGB ( '', 0.66274510, 0.83137255, 0.94901961) ;
#13612=( GEOMETRIC_REPRESENTATION_CONTEXT ( 3 ) GLOBAL_UNCERTAINTY_ASSIGNED_CONTEXT ( ( #8869 ) ) GLOBAL_UNIT_ASSIGNED_CONTEXT ( ( #17878, #463, #3670 ) ) REPRESENTATION_CONTEXT ( 'NONE', 'WORKASPACE' ) );
#13616=DIRECTION ( 'NONE',  ( 0.000000000000000000, 0.000000000000000000, 1.000000000000000000 ) ) ;
#13624=ORIENTED_EDGE ( 'NONE', *, *, #4475, .T. ) ;
#13628=DIRECTION ( 'NONE',  ( 0.000000000000000000, 1.000000000000000000, 0.000000000000000000 ) ) ;
#13641=UNCERTAINTY_MEASURE_WITH_UNIT (LENGTH_MEASURE( 1.000000000000000082E-05 ), #6012, 'distance_accuracy_value', 'NONE');
#13645=DIRECTION ( 'NONE',  ( 1.000000000000000000, 0.000000000000000000, 0.000000000000000000 ) ) ;
#13646=VECTOR ( 'NONE', #17514, 1000.000000000000000 ) ;
#13651=DIRECTION ( 'NONE',  ( 0.000000000000000000, 0.000000000000000000, -1.000000000000000000 ) ) ;
#13652=VECTOR ( 'NONE', #4923, 1000.000000000000000 ) ;
#13662=AXIS2_PLACEMENT_3D ( 'NONE', #3871, #1038, #13651 ) ;
#13664=EDGE_LOOP ( 'NONE', ( #7059, #18182, #1233, #7871 ) ) ;
#13665=( GEOMETRIC_REPRESENTATION_CONTEXT ( 3 ) GLOBAL_UNCERTAINTY_ASSIGNED_CONTEXT ( ( #8272 ) ) GLOBAL_UNIT_ASSIGNED_CONTEXT ( ( #16448, #16361, #17976 ) ) REPRESENTATION_CONTEXT ( 'NONE', 'WORKASPACE' ) );
#13686=VECTOR ( 'NONE', #15299, 1000.000000000000000 ) ;
#13687=SURFACE_STYLE_USAGE ( .BOTH. , #1069 ) ;
#13701=( LENGTH_UNIT ( ) NAMED_UNIT ( * ) SI_UNIT ( .MILLI., .METRE. ) );
#13702=CARTESIAN_POINT ( 'NONE',  ( 88.88953019741013861, 80.91625508013694912, 245.0000000000000000 ) ) ;
#13707=DIRECTION ( 'NONE',  ( 0.000000000000000000, 1.000000000000000000, 0.000000000000000000 ) ) ;
#13709=( NAMED_UNIT ( * ) PLANE_ANGLE_UNIT ( ) SI_UNIT ( $, .RADIAN. ) );
#13710=( NAMED_UNIT ( * ) SI_UNIT ( $, .STERADIAN. ) SOLID_ANGLE_UNIT ( ) );
#13737=VERTEX_POINT ( 'NONE', #629 ) ;
#13748=FILL_AREA_STYLE ('',( #13845 ) ) ;
#13761=CARTESIAN_POINT ( 'NONE',  ( 53.48937290013658696, 103.1299228374913923, 79.58252780074349175 ) ) ;
#13765=SURFACE_STYLE_FILL_AREA ( #15329 ) ;
#13766=DIRECTION ( 'NONE',  ( 1.000000000000000000, 2.135044278125300850E-16, -0.000000000000000000 ) ) ;
#13775=EDGE_CURVE ( 'NONE', #16217, #13442, #18184, .T. ) ;
#13778=ORIENTED_EDGE ( 'NONE', *, *, #4308, .T. ) ;
#13780=( NAMED_UNIT ( * ) SI_UNIT ( $, .STERADIAN. ) SOLID_ANGLE_UNIT ( ) );
#13789=CARTESIAN_POINT ( 'NONE',  ( -211.5106270998635409, 113.1299228374912502, 170.4174721992565082 ) ) ;
#13803=ORIENTED_EDGE ( 'NONE', *, *, #8489, .F. ) ;
#13818=STYLED_ITEM ( 'NONE', ( #18462 ), #5969 ) ;
#13819=EDGE_CURVE ( 'NONE', #16767, #18834, #13598, .T. ) ;
#13825=FILL_AREA_STYLE_COLOUR ( '', #19219 ) ;
#13830=COLOUR_RGB ( '', 0.72549020, 0.75294118, 0.79215686) ;
#13833=DIRECTION ( 'NONE',  ( 1.000000000000000000, 0.000000000000000000, 0.000000000000000000 ) ) ;
#13845=FILL_AREA_STYLE_COLOUR ( '', #16431 ) ;
#13859=( GEOMETRIC_REPRESENTATION_CONTEXT ( 3 ) GLOBAL_UNCERTAINTY_ASSIGNED_CONTEXT ( ( #8891 ) ) GLOBAL_UNIT_ASSIGNED_CONTEXT ( ( #7145, #11559, #8784 ) ) REPRESENTATION_CONTEXT ( 'NONE', 'WORKASPACE' ) );
#13864=CARTESIAN_POINT ( 'NONE',  ( -211.5106270998635409, 113.1299228374912502, 79.58252780074349175 ) ) ;
#13875=FACE_OUTER_BOUND ( 'NONE', #14442, .T. ) ;
#13878=EDGE_LOOP ( 'NONE', ( #6550, #7277, #4410, #44 ) ) ;
#13883=EDGE_LOOP ( 'NONE', ( #386, #18839, #13901, #3661, #3404, #6574 ) ) ;
#13884=DIRECTION ( 'NONE',  ( 1.000000000000000000, 0.000000000000000000, 0.000000000000000000 ) ) ;
#13888=LINE ( 'NONE', #6078, #16001 ) ;
#13890=VECTOR ( 'NONE', #2011, 1000.000000000000000 ) ;
#13901=ORIENTED_EDGE ( 'NONE', *, *, #1034, .F. ) ;
#13920=CARTESIAN_POINT ( 'NONE',  ( 53.48937290013658696, 123.1299228374914065, 220.6387154965113382 ) ) ;
#13930=CARTESIAN_POINT ( 'NONE',  ( 178.4893729001365728, 123.1299228374914918, 29.36128450348865471 ) ) ;
#13952=( NAMED_UNIT ( * ) PLANE_ANGLE_UNIT ( ) SI_UNIT ( $, .RADIAN. ) );
#13963=VECTOR ( 'NONE', #2625, 1000.000000000000000 ) ;
#13978=MECHANICAL_DESIGN_GEOMETRIC_PRESENTATION_REPRESENTATION('',(#18246),#5104);
#13979=DIRECTION ( 'NONE',  ( 0.000000000000000000, 0.000000000000000000, -1.000000000000000000 ) ) ;
#14002=ADVANCED_FACE ( 'NONE', ( #2491 ), #9174, .F. ) ;
#14006=CYLINDRICAL_SURFACE ( 'NONE', #8775, 10.00000000000000888 ) ;
#14010=DIRECTION ( 'NONE',  ( 1.000000000000000000, 5.889072920838430686E-16, -0.000000000000000000 ) ) ;
#14020=CARTESIAN_POINT ( 'NONE',  ( 98.48937290013660117, 80.91625508013694912, 250.0000000000000000 ) ) ;
#14023=EDGE_LOOP ( 'NONE', ( #15799, #12842, #18597, #10901 ) ) ;
#14026=VERTEX_POINT ( 'NONE', #13920 ) ;
#14033=EDGE_CURVE ( 'NONE', #8120, #3236, #3102, .T. ) ;
#14040=DIRECTION ( 'NONE',  ( 0.000000000000000000, 1.000000000000000000, 0.000000000000000000 ) ) ;
#14046=EDGE_LOOP ( 'NONE', ( #2752, #16699 ) ) ;
#14062=EDGE_CURVE ( 'NONE', #3302, #10482, #6713, .T. ) ;
#14081=DIRECTION ( 'NONE',  ( 0.000000000000000000, 1.000000000000000000, 0.000000000000000000 ) ) ;
#14082=( NAMED_UNIT ( * ) PLANE_ANGLE_UNIT ( ) SI_UNIT ( $, .RADIAN. ) );
#14090=VERTEX_POINT ( 'NONE', #18657 ) ;
#14097=DIRECTION ( 'NONE',  ( 1.000000000000000000, 0.000000000000000000, 0.000000000000000000 ) ) ;
#14101=CARTESIAN_POINT ( 'NONE',  ( 78.48937290013660117, 123.1299228374914208, 220.6387154965113382 ) ) ;
#14106=EDGE_CURVE ( 'NONE', #15780, #17589, #9482, .T. ) ;
#14108=ORIENTED_EDGE ( 'NONE', *, *, #15682, .F. ) ;
#14118=FILL_AREA_STYLE_COLOUR ( '', #13293 ) ;
#14127=DIRECTION ( 'NONE',  ( 0.000000000000000000, 1.000000000000000000, 0.000000000000000000 ) ) ;
#14138=LINE ( 'NONE', #23, #1751 ) ;
#14141=DIRECTION ( 'NONE',  ( 0.000000000000000000, -1.000000000000000000, 0.000000000000000000 ) ) ;
#14145=EDGE_CURVE ( 'NONE', #3589, #15013, #2073, .T. ) ;
#14146=( NAMED_UNIT ( * ) SI_UNIT ( $, .STERADIAN. ) SOLID_ANGLE_UNIT ( ) );
#14152=CARTESIAN_POINT ( 'NONE',  ( 153.4893729001366864, 113.1299228374914634, 79.58252780074349175 ) ) ;
#14169=ADVANCED_FACE ( 'NONE', ( #6828, #19455, #398, #2242, #8160 ), #3617, .F. ) ;
#14187=ORIENTED_EDGE ( 'NONE', *, *, #10228, .F. ) ;
#14190=ORIENTED_EDGE ( 'NONE', *, *, #16715, .F. ) ;
#14191=DIRECTION ( 'NONE',  ( 0.000000000000000000, 0.000000000000000000, -1.000000000000000000 ) ) ;
#14200=LINE ( 'NONE', #12774, #15404 ) ;
#14201=EDGE_CURVE ( 'NONE', #5831, #19951, #6369, .T. ) ;
#14210=ORIENTED_EDGE ( 'NONE', *, *, #15864, .T. ) ;
#14228=ORIENTED_EDGE ( 'NONE', *, *, #443, .F. ) ;
#14232=STYLED_ITEM ( 'NONE', ( #15536 ), #3321 ) ;
#14237=DIRECTION ( 'NONE',  ( 1.000000000000000000, 0.000000000000000000, 0.000000000000000000 ) ) ;
#14251=VECTOR ( 'NONE', #2932, 1000.000000000000000 ) ;
#14256=ORIENTED_EDGE ( 'NONE', *, *, #5348, .F. ) ;
#14260=EDGE_CURVE ( 'NONE', #10947, #10177, #2354, .T. ) ;
#14262=VERTEX_POINT ( 'NONE', #9226 ) ;
#14266=VECTOR ( 'NONE', #9153, 1000.000000000000000 ) ;
#14271=COLOUR_RGB ( '', 0.72549020, 0.75294118, 0.79215686) ;
#14297=DIRECTION ( 'NONE',  ( -1.000000000000000000, 0.000000000000000000, 0.000000000000000000 ) ) ;
#14298=ORIENTED_EDGE ( 'NONE', *, *, #9602, .F. ) ;
#14300=ORIENTED_EDGE ( 'NONE', *, *, #3445, .T. ) ;
#14301=STYLED_ITEM ( 'NONE', ( #9183 ), #19322 ) ;
#14311=LINE ( 'NONE', #7615, #14 ) ;
#14315=CIRCLE ( 'NONE', #13013, 10.00000000000000888 ) ;
#14341=ORIENTED_EDGE ( 'NONE', *, *, #11288, .T. ) ;
#14342=EDGE_CURVE ( 'NONE', #2874, #11813, #9059, .T. ) ;
#14343=CARTESIAN_POINT ( 'NONE',  ( 178.4893729001365443, 0.000000000000000000, 250.0000000000000000 ) ) ;
#14370=ORIENTED_EDGE ( 'NONE', *, *, #6887, .F. ) ;
#14374=CARTESIAN_POINT ( 'NONE',  ( 53.48937290013659407, 145.9162550801369491, -97.94896630388704750 ) ) ;
#14375=PRESENTATION_STYLE_ASSIGNMENT (( #12838 ) ) ;
#14381=FILL_AREA_STYLE_COLOUR ( '', #1970 ) ;
#14400=LINE ( 'NONE', #10802, #8955 ) ;
#14402=VERTEX_POINT ( 'NONE', #5010 ) ;
#14419=VERTEX_POINT ( 'NONE', #6557 ) ;
#14424=DIRECTION ( 'NONE',  ( -1.000000000000000000, 0.000000000000000000, 0.000000000000000000 ) ) ;
#14431=( NAMED_UNIT ( * ) PLANE_ANGLE_UNIT ( ) SI_UNIT ( $, .RADIAN. ) );
#14436=LINE ( 'NONE', #18856, #13646 ) ;
#14442=EDGE_LOOP ( 'NONE', ( #8823, #3783, #13566, #16747, #3293, #10312, #13778, #17673 ) ) ;
#14449=DIRECTION ( 'NONE',  ( 1.000000000000000000, 0.000000000000000000, 0.000000000000000000 ) ) ;
#14450=CIRCLE ( 'NONE', #6568, 10.00000000000000888 ) ;
#14451=EDGE_CURVE ( 'NONE', #4371, #6655, #5773, .T. ) ;
#14453=CARTESIAN_POINT ( 'NONE',  ( 78.48937290013660117, 123.1299228374914208, 29.36128450348865471 ) ) ;
#14456=ORIENTED_EDGE ( 'NONE', *, *, #9735, .T. ) ;
#14463=ORIENTED_EDGE ( 'NONE', *, *, #12946, .T. ) ;
#14464=VECTOR ( 'NONE', #10176, 1000.000000000000000 ) ;
#14467=STYLED_ITEM ( 'NONE', ( #15227 ), #5498 ) ;
#14468=VERTEX_POINT ( 'NONE', #1574 ) ;
#14473=DIRECTION ( 'NONE',  ( 0.000000000000000000, 1.000000000000000000, 0.000000000000000000 ) ) ;
#14477=CARTESIAN_POINT ( 'NONE',  ( 178.4893729001365728, 113.1299228374914918, 220.6387154965113382 ) ) ;
#14482=CARTESIAN_POINT ( 'NONE',  ( 78.48937290013660117, 113.1299228374914208, 29.36128450348865471 ) ) ;
#14490=VECTOR ( 'NONE', #5958, 1000.000000000000000 ) ;
#14500=LINE ( 'NONE', #12980, #1271 ) ;
#14509=ADVANCED_FACE ( 'NONE', ( #19501 ), #3869, .F. ) ;
#14512=LINE ( 'NONE', #2020, #14464 ) ;
#14519=EDGE_CURVE ( 'NONE', #16393, #6961, #11804, .T. ) ;
#14539=ORIENTED_EDGE ( 'NONE', *, *, #2961, .F. ) ;
#14540=CARTESIAN_POINT ( 'NONE',  ( 53.48937290013659407, 167.9162550801369491, 0.000000000000000000 ) ) ;
#14552=LINE ( 'NONE', #2378, #6857 ) ;
#14561=CIRCLE ( 'NONE', #17194, 10.00000000000000888 ) ;
#14566=ORIENTED_EDGE ( 'NONE', *, *, #9394, .F. ) ;
#14568=CYLINDRICAL_SURFACE ( 'NONE', #7048, 10.00000000000000888 ) ;
#14570=ORIENTED_EDGE ( 'NONE', *, *, #4038, .T. ) ;
#14605=ORIENTED_EDGE ( 'NONE', *, *, #13547, .T. ) ;
#14611=AXIS2_PLACEMENT_3D ( 'NONE', #19755, #12068, #13707 ) ;
#14621=FILL_AREA_STYLE_COLOUR ( '', #15464 ) ;
#14627=ORIENTED_EDGE ( 'NONE', *, *, #11532, .F. ) ;
#14631=AXIS2_PLACEMENT_3D ( 'NONE', #14482, #5318, #7993 ) ;
#14654=EDGE_CURVE ( 'NONE', #738, #14402, #19802, .T. ) ;
#14657=UNCERTAINTY_MEASURE_WITH_UNIT (LENGTH_MEASURE( 1.000000000000000082E-05 ), #14861, 'distance_accuracy_value', 'NONE');
#14658=DIRECTION ( 'NONE',  ( -0.000000000000000000, 0.000000000000000000, 1.000000000000000000 ) ) ;
#14668=FILL_AREA_STYLE ('',( #14862 ) ) ;
#14669=COLOUR_RGB ( '', 0.66274510, 0.83137255, 0.94901961) ;
#14671=LINE ( 'NONE', #11372, #7416 ) ;
#14696=ORIENTED_EDGE ( 'NONE', *, *, #11288, .F. ) ;
#14721=DIRECTION ( 'NONE',  ( 0.000000000000000000, 0.000000000000000000, -1.000000000000000000 ) ) ;
#14724=( NAMED_UNIT ( * ) SI_UNIT ( $, .STERADIAN. ) SOLID_ANGLE_UNIT ( ) );
#14736=AXIS2_PLACEMENT_3D ( 'NONE', #4985, #3011, #12820 ) ;
#14742=CARTESIAN_POINT ( 'NONE',  ( 149.0892156028631348, 80.91625508013694912, 245.0000000000000000 ) ) ;
#14750=DIRECTION ( 'NONE',  ( 0.000000000000000000, 0.000000000000000000, 1.000000000000000000 ) ) ;
#14752=CYLINDRICAL_SURFACE ( 'NONE', #6238, 10.00000000000000888 ) ;
#14758=PLANE ( 'NONE',  #15158 ) ;
#14762=PRESENTATION_STYLE_ASSIGNMENT (( #17658 ) ) ;
#14774=ORIENTED_EDGE ( 'NONE', *, *, #16210, .T. ) ;
#14784=DIRECTION ( 'NONE',  ( 0.000000000000000000, 0.000000000000000000, -1.000000000000000000 ) ) ;
#14795=EDGE_LOOP ( 'NONE', ( #13001, #15130, #17744, #17403 ) ) ;
#14802=DIRECTION ( 'NONE',  ( 1.000000000000000000, -0.000000000000000000, -0.000000000000000000 ) ) ;
#14810=DIRECTION ( 'NONE',  ( 0.000000000000000000, -1.000000000000000000, 0.000000000000000000 ) ) ;
#14813=( NAMED_UNIT ( * ) PLANE_ANGLE_UNIT ( ) SI_UNIT ( $, .RADIAN. ) );
#14819=ORIENTED_EDGE ( 'NONE', *, *, #19544, .F. ) ;
#14824=CYLINDRICAL_SURFACE ( 'NONE', #12997, 10.00000000000000888 ) ;
#14825=CARTESIAN_POINT ( 'NONE',  ( 53.48937290013659407, 145.9162550801369491, 250.0000000000000000 ) ) ;
#14829=( GEOMETRIC_REPRESENTATION_CONTEXT ( 3 ) GLOBAL_UNCERTAINTY_ASSIGNED_CONTEXT ( ( #2253 ) ) GLOBAL_UNIT_ASSIGNED_CONTEXT ( ( #1235, #6025, #14146 ) ) REPRESENTATION_CONTEXT ( 'NONE', 'WORKASPACE' ) );
#14830=EDGE_CURVE ( 'NONE', #5907, #1869, #19902, .T. ) ;
#14841=DIRECTION ( 'NONE',  ( 1.000000000000000000, 0.000000000000000000, 0.000000000000000000 ) ) ;
#14842=LINE ( 'NONE', #707, #2112 ) ;
#14846=CIRCLE ( 'NONE', #20102, 10.00000000000000888 ) ;
#14853=ADVANCED_FACE ( 'NONE', ( #19189 ), #13341, .F. ) ;
#14861=( LENGTH_UNIT ( ) NAMED_UNIT ( * ) SI_UNIT ( .MILLI., .METRE. ) );
#14862=FILL_AREA_STYLE_COLOUR ( '', #13444 ) ;
#14866=ORIENTED_EDGE ( 'NONE', *, *, #15471, .F. ) ;
#14876=CARTESIAN_POINT ( 'NONE',  ( -211.5106270998635409, 123.1299228374912644, 79.58252780074349175 ) ) ;
#14882=CARTESIAN_POINT ( 'NONE',  ( -211.5106270998635409, 103.1299228374912360, 29.36128450348865471 ) ) ;
#14891=AXIS2_PLACEMENT_3D ( 'NONE', #7998, #17162, #163 ) ;
#14920=DIRECTION ( 'NONE',  ( -1.000000000000000000, -2.135044278125301096E-16, -0.000000000000000000 ) ) ;
#14925=( NAMED_UNIT ( * ) PLANE_ANGLE_UNIT ( ) SI_UNIT ( $, .RADIAN. ) );
#14942=VECTOR ( 'NONE', #11206, 1000.000000000000000 ) ;
#14949=DIRECTION ( 'NONE',  ( -5.889072920838430686E-16, 1.000000000000000000, -0.000000000000000000 ) ) ;
#14959=COLOUR_RGB ( '', 0.72549020, 0.75294118, 0.79215686) ;
#14964=ORIENTED_EDGE ( 'NONE', *, *, #16300, .F. ) ;
#14967=FACE_OUTER_BOUND ( 'NONE', #15405, .T. ) ;
#14978=FACE_OUTER_BOUND ( 'NONE', #8683, .T. ) ;
#14982=EDGE_CURVE ( 'NONE', #14090, #16534, #2888, .T. ) ;
#14986=VECTOR ( 'NONE', #18608, 1000.000000000000000 ) ;
#14993=ORIENTED_EDGE ( 'NONE', *, *, #5329, .F. ) ;
#14994=FILL_AREA_STYLE_COLOUR ( '', #4427 ) ;
#15009=ORIENTED_EDGE ( 'NONE', *, *, #847, .T. ) ;
#15013=VERTEX_POINT ( 'NONE', #6308 ) ;
#15015=DIRECTION ( 'NONE',  ( 0.000000000000000000, 0.000000000000000000, -1.000000000000000000 ) ) ;
#15026=MECHANICAL_DESIGN_GEOMETRIC_PRESENTATION_REPRESENTATION('',(#5478),#16034);
#15037=EDGE_LOOP ( 'NONE', ( #8298, #17400 ) ) ;
#15041=DIRECTION ( 'NONE',  ( 1.000000000000000000, 5.889072920838430686E-16, -0.000000000000000000 ) ) ;
#15047=LINE ( 'NONE', #11956, #10118 ) ;
#15058=ORIENTED_EDGE ( 'NONE', *, *, #11177, .F. ) ;
#15065=FILL_AREA_STYLE_COLOUR ( '', #20363 ) ;
#15086=UNCERTAINTY_MEASURE_WITH_UNIT (LENGTH_MEASURE( 1.000000000000000082E-05 ), #10448, 'distance_accuracy_value', 'NONE');
#15089=FACE_OUTER_BOUND ( 'NONE', #15826, .T. ) ;
#15093=EDGE_CURVE ( 'NONE', #14419, #13737, #9801, .T. ) ;
#15095=CARTESIAN_POINT ( 'NONE',  ( 78.48937290013661539, 80.91625508013694912, -140.0000000000001137 ) ) ;
#15096=CARTESIAN_POINT ( 'NONE',  ( 0.000000000000000000, 80.91625508013694912, -97.94896630388704750 ) ) ;
#15105=CIRCLE ( 'NONE', #6224, 10.00000000000000888 ) ;
#15108=VERTEX_POINT ( 'NONE', #4471 ) ;
#15130=ORIENTED_EDGE ( 'NONE', *, *, #14106, .T. ) ;
#15145=SURFACE_STYLE_FILL_AREA ( #4321 ) ;
#15147=VECTOR ( 'NONE', #15502, 1000.000000000000000 ) ;
#15158=AXIS2_PLACEMENT_3D ( 'NONE', #6852, #9723, #542 ) ;
#15185=EDGE_LOOP ( 'NONE', ( #19446, #12182, #9940, #10630 ) ) ;
#15187=( NAMED_UNIT ( * ) SI_UNIT ( $, .STERADIAN. ) SOLID_ANGLE_UNIT ( ) );
#15194=DIRECTION ( 'NONE',  ( 0.000000000000000000, -1.000000000000000000, 0.000000000000000000 ) ) ;
#15200=ADVANCED_FACE ( 'NONE', ( #11063 ), #7858, .F. ) ;
#15205=CIRCLE ( 'NONE', #19134, 10.00000000000000888 ) ;
#15227=PRESENTATION_STYLE_ASSIGNMENT (( #13687 ) ) ;
#15247=FACE_OUTER_BOUND ( 'NONE', #15574, .T. ) ;
#15249=FILL_AREA_STYLE ('',( #13502 ) ) ;
#15252=VECTOR ( 'NONE', #19051, 1000.000000000000000 ) ;
#15269=STYLED_ITEM ( 'NONE', ( #20003 ), #1329 ) ;
#15271=COLOUR_RGB ( '', 0.08235294, 0.09019608, 0.10196078) ;
#15285=STYLED_ITEM ( 'NONE', ( #12719 ), #1368 ) ;
#15294=( GEOMETRIC_REPRESENTATION_CONTEXT ( 3 ) GLOBAL_UNCERTAINTY_ASSIGNED_CONTEXT ( ( #19982 ) ) GLOBAL_UNIT_ASSIGNED_CONTEXT ( ( #8059, #10945, #10740 ) ) REPRESENTATION_CONTEXT ( 'NONE', 'WORKASPACE' ) );
#15296=UNCERTAINTY_MEASURE_WITH_UNIT (LENGTH_MEASURE( 1.000000000000000082E-05 ), #15887, 'distance_accuracy_value', 'NONE');
#15299=DIRECTION ( 'NONE',  ( -0.000000000000000000, -0.000000000000000000, -1.000000000000000000 ) ) ;
#15300=FILL_AREA_STYLE ('',( #13457 ) ) ;
#15305=EDGE_LOOP ( 'NONE', ( #11239, #19148 ) ) ;
#15306=ADVANCED_FACE ( 'NONE', ( #2133 ), #379, .F. ) ;
#15312=FILL_AREA_STYLE_COLOUR ( '', #5667 ) ;
#15324=VECTOR ( 'NONE', #19822, 1000.000000000000000 ) ;
#15329=FILL_AREA_STYLE ('',( #12039 ) ) ;
#15332=COLOUR_RGB ( '', 0.09019608, 0.27058824, 0.51372549) ;
#15341=SURFACE_STYLE_USAGE ( .BOTH. , #12340 ) ;
#15343=CARTESIAN_POINT ( 'NONE',  ( 0.000000000000000000, 167.9162550801369491, 0.000000000000000000 ) ) ;
#15360=FACE_OUTER_BOUND ( 'NONE', #9216, .T. ) ;
#15362=DIRECTION ( 'NONE',  ( -1.000000000000000000, 0.000000000000000000, 0.000000000000000000 ) ) ;
#15371=ORIENTED_EDGE ( 'NONE', *, *, #17823, .T. ) ;
#15376=( LENGTH_UNIT ( ) NAMED_UNIT ( * ) SI_UNIT ( .MILLI., .METRE. ) );
#15389=LINE ( 'NONE', #11988, #9342 ) ;
#15395=ORIENTED_EDGE ( 'NONE', *, *, #17823, .F. ) ;
#15404=VECTOR ( 'NONE', #1828, 1000.000000000000000 ) ;
#15405=EDGE_LOOP ( 'NONE', ( #674, #14256, #13624, #4891 ) ) ;
#15407=CARTESIAN_POINT ( 'NONE',  ( 153.4893729001366580, 145.9162550801369491, 250.0000000000000000 ) ) ;
#15412=PRODUCT_DEFINITION ( 'UNKNOWN', '', #3044, #8636 ) ;
#15425=SURFACE_SIDE_STYLE ('',( #13765 ) ) ;
#15447=ORIENTED_EDGE ( 'NONE', *, *, #13775, .T. ) ;
#15450=SURFACE_SIDE_STYLE ('',( #12841 ) ) ;
#15459=CYLINDRICAL_SURFACE ( 'NONE', #18855, 10.00000000000000888 ) ;
#15464=COLOUR_RGB ( '', 0.66274510, 0.83137255, 0.94901961) ;
#15471=EDGE_CURVE ( 'NONE', #530, #738, #6362, .T. ) ;
#15481=( NAMED_UNIT ( * ) PLANE_ANGLE_UNIT ( ) SI_UNIT ( $, .RADIAN. ) );
#15500=EDGE_LOOP ( 'NONE', ( #6296, #18179 ) ) ;
#15502=DIRECTION ( 'NONE',  ( 2.135044278125300850E-16, -1.000000000000000000, 0.000000000000000000 ) ) ;
#15504=LINE ( 'NONE', #15913, #19909 ) ;
#15507=AXIS2_PLACEMENT_3D ( 'NONE', #2302, #3970, #8906 ) ;
#15509=STYLED_ITEM ( 'NONE', ( #19101 ), #7251 ) ;
#15512=CARTESIAN_POINT ( 'NONE',  ( -211.5106270998635409, 103.1299228374912360, 79.58252780074349175 ) ) ;
#15524=EDGE_CURVE ( 'NONE', #5614, #2877, #18915, .T. ) ;
#15535=CARTESIAN_POINT ( 'NONE',  ( 98.48937290013662960, 103.1299228374914208, 29.36128450348865471 ) ) ;
#15536=PRESENTATION_STYLE_ASSIGNMENT (( #10778 ) ) ;
#15544=DIRECTION ( 'NONE',  ( 2.135044278125301096E-16, -1.000000000000000000, 0.000000000000000000 ) ) ;
#15548=EDGE_LOOP ( 'NONE', ( #16017, #19271, #15903, #16773 ) ) ;
#15550=EDGE_CURVE ( 'NONE', #14419, #15780, #13141, .T. ) ;
#15555=DIRECTION ( 'NONE',  ( 1.000000000000000000, 5.889072920838430686E-16, -0.000000000000000000 ) ) ;
#15564=DIRECTION ( 'NONE',  ( 0.000000000000000000, 1.000000000000000000, 0.000000000000000000 ) ) ;
#15565=FILL_AREA_STYLE_COLOUR ( '', #17882 ) ;
#15574=EDGE_LOOP ( 'NONE', ( #7875, #14300, #12319, #11916 ) ) ;
#15576=DIRECTION ( 'NONE',  ( 0.000000000000000000, 1.000000000000000000, 0.000000000000000000 ) ) ;
#15581=AXIS2_PLACEMENT_3D ( 'NONE', #11881, #2494, #18552 ) ;
#15592=DIRECTION ( 'NONE',  ( -0.000000000000000000, -1.000000000000000000, -0.000000000000000000 ) ) ;
#15593=CARTESIAN_POINT ( 'NONE',  ( 133.4893729001365443, 123.1299228374914634, 170.4174721992565082 ) ) ;
#15609=SURFACE_STYLE_FILL_AREA ( #3002 ) ;
#15627=ORIENTED_EDGE ( 'NONE', *, *, #4308, .F. ) ;
#15633=CIRCLE ( 'NONE', #14631, 10.00000000000000888 ) ;
#15647=DIRECTION ( 'NONE',  ( -1.000000000000000000, -5.889072920838430686E-16, 0.000000000000000000 ) ) ;
#15658=VERTEX_POINT ( 'NONE', #8115 ) ;
#15661=COLOUR_RGB ( '', 0.40784314, 0.44705882, 0.49803922) ;
#15666=CARTESIAN_POINT ( 'NONE',  ( 78.48937290013660117, 145.9162550801369491, -140.0000000000001137 ) ) ;
#15680=LINE ( 'NONE', #7722, #9543 ) ;
#15682=EDGE_CURVE ( 'NONE', #995, #19309, #19004, .T. ) ;
#15683=ORIENTED_EDGE ( 'NONE', *, *, #9804, .F. ) ;
#15697=CARTESIAN_POINT ( 'NONE',  ( -211.5106270998635409, 113.1299228374912502, 220.6387154965113382 ) ) ;
#15714=( LENGTH_UNIT ( ) NAMED_UNIT ( * ) SI_UNIT ( .MILLI., .METRE. ) );
#15718=CARTESIAN_POINT ( 'NONE',  ( 78.48937290013662960, 1.675782865040797740E-14, 0.000000000000000000 ) ) ;
#15726=ORIENTED_EDGE ( 'NONE', *, *, #12395, .T. ) ;
#15727=CARTESIAN_POINT ( 'NONE',  ( 78.48937290013660117, 123.1299228374914208, 79.58252780074349175 ) ) ;
#15737=ADVANCED_FACE ( 'NONE', ( #10838 ), #16931, .F. ) ;
#15748=FILL_AREA_STYLE ('',( #1890 ) ) ;
#15764=CARTESIAN_POINT ( 'NONE',  ( 153.4893729001366864, 103.1299228374914492, 79.58252780074349175 ) ) ;
#15769=FILL_AREA_STYLE ('',( #12668 ) ) ;
#15770=AXIS2_PLACEMENT_3D ( 'NONE', #1040, #15194, #7565 ) ;
#15780=VERTEX_POINT ( 'NONE', #12 ) ;
#15784=DIRECTION ( 'NONE',  ( 1.000000000000000000, 5.889072920838430686E-16, -0.000000000000000000 ) ) ;
#15785=LINE ( 'NONE', #15888, #5643 ) ;
#15788=DIRECTION ( 'NONE',  ( -0.000000000000000000, 1.000000000000000000, 0.000000000000000000 ) ) ;
#15794=ORIENTED_EDGE ( 'NONE', *, *, #819, .T. ) ;
#15799=ORIENTED_EDGE ( 'NONE', *, *, #10125, .F. ) ;
#15801=EDGE_CURVE ( 'NONE', #39, #20118, #15900, .T. ) ;
#15808=( NAMED_UNIT ( * ) PLANE_ANGLE_UNIT ( ) SI_UNIT ( $, .RADIAN. ) );
#15817=CARTESIAN_POINT ( 'NONE',  ( 0.000000000000000000, 0.000000000000000000, 250.0000000000000000 ) ) ;
#15819=DIRECTION ( 'NONE',  ( 0.000000000000000000, 0.000000000000000000, -1.000000000000000000 ) ) ;
#15820=AXIS2_PLACEMENT_3D ( 'NONE', #18373, #5521, #4274 ) ;
#15824=CIRCLE ( 'NONE', #16162, 10.00000000000000888 ) ;
#15826=EDGE_LOOP ( 'NONE', ( #5021, #16135, #5138, #19249, #2251, #9101, #7932, #17861 ) ) ;
#15828=EDGE_CURVE ( 'NONE', #11725, #6461, #14436, .T. ) ;
#15837=FILL_AREA_STYLE ('',( #9622 ) ) ;
#15839=STYLED_ITEM ( 'NONE', ( #9814 ), #7362 ) ;
#15843=SURFACE_SIDE_STYLE ('',( #18904 ) ) ;
#15853=CARTESIAN_POINT ( 'NONE',  ( 178.4893729001365728, 113.1299228374914918, 79.58252780074349175 ) ) ;
#15857=VECTOR ( 'NONE', #16820, 1000.000000000000000 ) ;
#15858=VERTEX_POINT ( 'NONE', #8163 ) ;
#15863=DIRECTION ( 'NONE',  ( 0.000000000000000000, 1.000000000000000000, 0.000000000000000000 ) ) ;
#15864=EDGE_CURVE ( 'NONE', #6099, #18945, #8056, .T. ) ;
#15869=CARTESIAN_POINT ( 'NONE',  ( 153.4893729001366580, 0.000000000000000000, -97.94896630388704750 ) ) ;
#15878=DIRECTION ( 'NONE',  ( 0.000000000000000000, 0.000000000000000000, -1.000000000000000000 ) ) ;
#15879=EDGE_LOOP ( 'NONE', ( #11319, #6915, #11884, #14341 ) ) ;
#15887=( LENGTH_UNIT ( ) NAMED_UNIT ( * ) SI_UNIT ( .MILLI., .METRE. ) );
#15888=CARTESIAN_POINT ( 'NONE',  ( 149.0892156028631348, 167.9162550801369491, 245.0000000000000000 ) ) ;
#15896=CARTESIAN_POINT ( 'NONE',  ( 178.4893729001366012, 34.32473510485366575, -140.0000000000001137 ) ) ;
#15900=LINE ( 'NONE', #14343, #1437 ) ;
#15903=ORIENTED_EDGE ( 'NONE', *, *, #10485, .F. ) ;
#15906=EDGE_CURVE ( 'NONE', #19309, #10163, #9703, .T. ) ;
#15907=CYLINDRICAL_SURFACE ( 'NONE', #12191, 10.00000000000000888 ) ;
#15913=CARTESIAN_POINT ( 'NONE',  ( 153.4893729001366580, 80.91625508013694912, -97.94896630388704750 ) ) ;
#15928=EDGE_CURVE ( 'NONE', #13587, #2876, #3780, .T. ) ;
#15930=ORIENTED_EDGE ( 'NONE', *, *, #10136, .F. ) ;
#15942=MECHANICAL_DESIGN_GEOMETRIC_PRESENTATION_REPRESENTATION('',(#8025),#13612);
#15957=DIRECTION ( 'NONE',  ( -9.815121534730717399E-17, 1.000000000000000000, 0.000000000000000000 ) ) ;
#15962=STYLED_ITEM ( 'NONE', ( #10141 ), #10198 ) ;
#15968=ORIENTED_EDGE ( 'NONE', *, *, #14201, .T. ) ;
#15982=EDGE_CURVE ( 'NONE', #8633, #3886, #16948, .T. ) ;
#15986=AXIS2_PLACEMENT_3D ( 'NONE', #16235, #7965, #16039 ) ;
#15987=CARTESIAN_POINT ( 'NONE',  ( 178.4893729001365728, 103.1299228374914776, 79.58252780074349175 ) ) ;
#15989=FACE_BOUND ( 'NONE', #447, .T. ) ;
#15997=CIRCLE ( 'NONE', #7088, 10.00000000000000888 ) ;
#16000=ORIENTED_EDGE ( 'NONE', *, *, #9385, .T. ) ;
#16001=VECTOR ( 'NONE', #1508, 1000.000000000000000 ) ;
#16003=ORIENTED_EDGE ( 'NONE', *, *, #19145, .F. ) ;
#16007=ORIENTED_EDGE ( 'NONE', *, *, #1293, .T. ) ;
#16017=ORIENTED_EDGE ( 'NONE', *, *, #14033, .T. ) ;
#16027=DIRECTION ( 'NONE',  ( 0.000000000000000000, 1.000000000000000000, 0.000000000000000000 ) ) ;
#16028=VERTEX_POINT ( 'NONE', #7316 ) ;
#16034=( GEOMETRIC_REPRESENTATION_CONTEXT ( 3 ) GLOBAL_UNCERTAINTY_ASSIGNED_CONTEXT ( ( #11705 ) ) GLOBAL_UNIT_ASSIGNED_CONTEXT ( ( #2654, #7512, #13780 ) ) REPRESENTATION_CONTEXT ( 'NONE', 'WORKASPACE' ) );
#16039=DIRECTION ( 'NONE',  ( 0.000000000000000000, 1.000000000000000000, 0.000000000000000000 ) ) ;
#16050=ORIENTED_EDGE ( 'NONE', *, *, #8727, .F. ) ;
#16064=( NAMED_UNIT ( * ) SI_UNIT ( $, .STERADIAN. ) SOLID_ANGLE_UNIT ( ) );
#16088=DIRECTION ( 'NONE',  ( 0.000000000000000000, 0.000000000000000000, -1.000000000000000000 ) ) ;
#16095=FILL_AREA_STYLE_COLOUR ( '', #19105 ) ;
#16099=EDGE_LOOP ( 'NONE', ( #16670, #14210, #13465, #15009 ) ) ;
#16128=FACE_BOUND ( 'NONE', #2977, .T. ) ;
#16135=ORIENTED_EDGE ( 'NONE', *, *, #3957, .T. ) ;
#16145=( GEOMETRIC_REPRESENTATION_CONTEXT ( 3 ) GLOBAL_UNCERTAINTY_ASSIGNED_CONTEXT ( ( #8526 ) ) GLOBAL_UNIT_ASSIGNED_CONTEXT ( ( #1369, #10479, #2746 ) ) REPRESENTATION_CONTEXT ( 'NONE', 'WORKASPACE' ) );
#16149=FACE_OUTER_BOUND ( 'NONE', #13244, .T. ) ;
#16151=UNCERTAINTY_MEASURE_WITH_UNIT (LENGTH_MEASURE( 1.000000000000000082E-05 ), #8626, 'distance_accuracy_value', 'NONE');
#16152=DIRECTION ( 'NONE',  ( -2.135044278125300850E-16, 1.000000000000000000, 0.000000000000000000 ) ) ;
#16156=CARTESIAN_POINT ( 'NONE',  ( 88.88953019741013861, 167.9162550801369491, 245.0000000000000000 ) ) ;
#16162=AXIS2_PLACEMENT_3D ( 'NONE', #11060, #17126, #10747 ) ;
#16173=STYLED_ITEM ( 'NONE', ( #8857 ), #16557 ) ;
#16182=EDGE_CURVE ( 'NONE', #12453, #17965, #3932, .T. ) ;
#16191=DIRECTION ( 'NONE',  ( 1.000000000000000000, 5.889072920838430686E-16, -0.000000000000000000 ) ) ;
#16193=ADVANCED_FACE ( 'NONE', ( #1719 ), #8030, .F. ) ;
#16194=ORIENTED_EDGE ( 'NONE', *, *, #13547, .F. ) ;
#16210=EDGE_CURVE ( 'NONE', #7788, #3926, #14512, .T. ) ;
#16217=VERTEX_POINT ( 'NONE', #19265 ) ;
#16223=CARTESIAN_POINT ( 'NONE',  ( -211.5106270998635409, 113.1299228374912502, 29.36128450348865471 ) ) ;
#16227=ADVANCED_FACE ( 'NONE', ( #10089 ), #3603, .F. ) ;
#16231=CIRCLE ( 'NONE', #16876, 10.00000000000000888 ) ;
#16235=CARTESIAN_POINT ( 'NONE',  ( -211.5106270998635409, 113.1299228374912502, 220.6387154965113382 ) ) ;
#16240=FILL_AREA_STYLE_COLOUR ( '', #14959 ) ;
#16247=EDGE_LOOP ( 'NONE', ( #3456, #16900, #12914, #10087 ) ) ;
#16254=EDGE_LOOP ( 'NONE', ( #9983, #6767 ) ) ;
#16260=SURFACE_STYLE_FILL_AREA ( #654 ) ;
#16264=DIRECTION ( 'NONE',  ( 0.000000000000000000, 0.000000000000000000, 1.000000000000000000 ) ) ;
#16283=COLOUR_RGB ( '', 0.66274510, 0.83137255, 0.94901961) ;
#16299=COLOUR_RGB ( '', 0.40784314, 0.44705882, 0.49803922) ;
#16300=EDGE_CURVE ( 'NONE', #3638, #17811, #7503, .T. ) ;
#16333=UNCERTAINTY_MEASURE_WITH_UNIT (LENGTH_MEASURE( 1.000000000000000082E-05 ), #6563, 'distance_accuracy_value', 'NONE');
#16338=DIRECTION ( 'NONE',  ( 1.000000000000000000, 5.889072920838430686E-16, 0.000000000000000000 ) ) ;
#16340=PRESENTATION_STYLE_ASSIGNMENT (( #11467 ) ) ;
#16341=( GEOMETRIC_REPRESENTATION_CONTEXT ( 3 ) GLOBAL_UNCERTAINTY_ASSIGNED_CONTEXT ( ( #9917 ) ) GLOBAL_UNIT_ASSIGNED_CONTEXT ( ( #7237, #2171, #19773 ) ) REPRESENTATION_CONTEXT ( 'NONE', 'WORKASPACE' ) );
#16345=ORIENTED_EDGE ( 'NONE', *, *, #6887, .T. ) ;
#16360=DIRECTION ( 'NONE',  ( -0.000000000000000000, -0.000000000000000000, 1.000000000000000000 ) ) ;
#16361=( NAMED_UNIT ( * ) PLANE_ANGLE_UNIT ( ) SI_UNIT ( $, .RADIAN. ) );
#16370=PLANE ( 'NONE',  #12626 ) ;
#16393=VERTEX_POINT ( 'NONE', #17076 ) ;
#16395=SURFACE_SIDE_STYLE ('',( #1918 ) ) ;
#16403=FACE_OUTER_BOUND ( 'NONE', #18967, .T. ) ;
#16408=FILL_AREA_STYLE_COLOUR ( '', #13611 ) ;
#16413=DIRECTION ( 'NONE',  ( 0.000000000000000000, 0.000000000000000000, -1.000000000000000000 ) ) ;
#16417=VECTOR ( 'NONE', #7801, 1000.000000000000000 ) ;
#16429=CARTESIAN_POINT ( 'NONE',  ( -211.5106270998635409, 123.1299228374912644, 29.36128450348865471 ) ) ;
#16431=COLOUR_RGB ( '', 0.09019608, 0.27058824, 0.51372549) ;
#16437=ORIENTED_EDGE ( 'NONE', *, *, #1668, .T. ) ;
#16438=EDGE_CURVE ( 'NONE', #12058, #17253, #1373, .T. ) ;
#16439=VECTOR ( 'NONE', #13460, 1000.000000000000000 ) ;
#16445=LINE ( 'NONE', #17562, #7741 ) ;
#16446=CARTESIAN_POINT ( 'NONE',  ( -211.5106270998635409, 113.1299228374912502, 79.58252780074349175 ) ) ;
#16448=( LENGTH_UNIT ( ) NAMED_UNIT ( * ) SI_UNIT ( .MILLI., .METRE. ) );
#16464=ORIENTED_EDGE ( 'NONE', *, *, #20106, .T. ) ;
#16467=DIRECTION ( 'NONE',  ( 0.000000000000000000, -1.000000000000000000, 0.000000000000000000 ) ) ;
#16470=VECTOR ( 'NONE', #16683, 1000.000000000000000 ) ;
#16473=LINE ( 'NONE', #8831, #16470 ) ;
#16480=FACE_OUTER_BOUND ( 'NONE', #14023, .T. ) ;
#16492=DIRECTION ( 'NONE',  ( 1.000000000000000000, 9.815121534730717399E-17, -0.000000000000000000 ) ) ;
#16494=DIRECTION ( 'NONE',  ( 0.000000000000000000, 1.000000000000000000, 0.000000000000000000 ) ) ;
#16500=CARTESIAN_POINT ( 'NONE',  ( 153.4893729001366864, 113.1299228374914634, 29.36128450348865471 ) ) ;
#16501=( NAMED_UNIT ( * ) PLANE_ANGLE_UNIT ( ) SI_UNIT ( $, .RADIAN. ) );
#16515=ORIENTED_EDGE ( 'NONE', *, *, #7227, .F. ) ;
#16532=CARTESIAN_POINT ( 'NONE',  ( 153.4893729001366580, 0.000000000000000000, 0.000000000000000000 ) ) ;
#16534=VERTEX_POINT ( 'NONE', #9070 ) ;
#16557=ADVANCED_FACE ( 'NONE', ( #5877 ), #2866, .F. ) ;
#16558=SURFACE_STYLE_USAGE ( .BOTH. , #7484 ) ;
#16560=ORIENTED_EDGE ( 'NONE', *, *, #16735, .F. ) ;
#16591=VECTOR ( 'NONE', #17820, 1000.000000000000000 ) ;
#16599=VERTEX_POINT ( 'NONE', #12777 ) ;
#16602=DIRECTION ( 'NONE',  ( 0.000000000000000000, 0.000000000000000000, 1.000000000000000000 ) ) ;
#16606=MECHANICAL_DESIGN_GEOMETRIC_PRESENTATION_REPRESENTATION('',(#1204),#11640);
#16607=AXIS2_PLACEMENT_3D ( 'NONE', #9313, #3444, #15819 ) ;
#16611=DIRECTION ( 'NONE',  ( 0.000000000000000000, 0.000000000000000000, -1.000000000000000000 ) ) ;
#16613=FACE_OUTER_BOUND ( 'NONE', #20001, .T. ) ;
#16615=( GEOMETRIC_REPRESENTATION_CONTEXT ( 3 ) GLOBAL_UNCERTAINTY_ASSIGNED_CONTEXT ( ( #13641 ) ) GLOBAL_UNIT_ASSIGNED_CONTEXT ( ( #6012, #18576, #4469 ) ) REPRESENTATION_CONTEXT ( 'NONE', 'WORKASPACE' ) );
#16627=EDGE_LOOP ( 'NONE', ( #15395, #5206, #14605, #10230 ) ) ;
#16628=EDGE_CURVE ( 'NONE', #11436, #270, #14311, .T. ) ;
#16633=FILL_AREA_STYLE ('',( #6941 ) ) ;
#16634=AXIS2_PLACEMENT_3D ( 'NONE', #3737, #14658, #13129 ) ;
#16636=LINE ( 'NONE', #1116, #2447 ) ;
#16647=DIRECTION ( 'NONE',  ( 1.000000000000000000, 5.889072920838430686E-16, -0.000000000000000000 ) ) ;
#16650=EDGE_CURVE ( 'NONE', #11661, #11725, #15680, .T. ) ;
#16655=CARTESIAN_POINT ( 'NONE',  ( 53.48937290013659407, 145.9162550801369491, 0.000000000000000000 ) ) ;
#16669=DIRECTION ( 'NONE',  ( 1.000000000000000000, 5.889072920838430686E-16, -0.000000000000000000 ) ) ;
#16670=ORIENTED_EDGE ( 'NONE', *, *, #7969, .T. ) ;
#16678=LINE ( 'NONE', #13564, #15324 ) ;
#16683=DIRECTION ( 'NONE',  ( -0.000000000000000000, 1.000000000000000000, -0.000000000000000000 ) ) ;
#16690=CARTESIAN_POINT ( 'NONE',  ( 153.4893729001366864, 103.1299228374914492, 220.6387154965113382 ) ) ;
#16699=ORIENTED_EDGE ( 'NONE', *, *, #7116, .T. ) ;
#16700=UNCERTAINTY_MEASURE_WITH_UNIT (LENGTH_MEASURE( 1.000000000000000082E-05 ), #11287, 'distance_accuracy_value', 'NONE');
#16714=DIRECTION ( 'NONE',  ( 0.000000000000000000, 1.000000000000000000, 0.000000000000000000 ) ) ;
#16715=EDGE_CURVE ( 'NONE', #18945, #8120, #946, .T. ) ;
#16732=SURFACE_STYLE_FILL_AREA ( #16633 ) ;
#16735=EDGE_CURVE ( 'NONE', #345, #7788, #7265, .T. ) ;
#16742=CARTESIAN_POINT ( 'NONE',  ( 0.000000000000000000, 0.000000000000000000, 0.000000000000000000 ) ) ;
#16743=CARTESIAN_POINT ( 'NONE',  ( -211.5106270998635409, 123.1299228374912644, 170.4174721992565082 ) ) ;
#16747=ORIENTED_EDGE ( 'NONE', *, *, #1668, .F. ) ;
#16753=CARTESIAN_POINT ( 'NONE',  ( 0.000000000000000000, 80.91625508013694912, -97.94896630388704750 ) ) ;
#16760=PRESENTATION_STYLE_ASSIGNMENT (( #18587 ) ) ;
#16762=FILL_AREA_STYLE ('',( #756 ) ) ;
#16767=VERTEX_POINT ( 'NONE', #2519 ) ;
#16771=ORIENTED_EDGE ( 'NONE', *, *, #5718, .F. ) ;
#16773=ORIENTED_EDGE ( 'NONE', *, *, #16715, .T. ) ;
#16782=SURFACE_STYLE_FILL_AREA ( #6168 ) ;
#16783=CARTESIAN_POINT ( 'NONE',  ( 133.4893729001365728, 0.000000000000000000, 250.0000000000000000 ) ) ;
#16790=EDGE_CURVE ( 'NONE', #20243, #14026, #6610, .T. ) ;
#16791=SURFACE_SIDE_STYLE ('',( #10799 ) ) ;
#16801=DIRECTION ( 'NONE',  ( 0.000000000000000000, 0.000000000000000000, 1.000000000000000000 ) ) ;
#16815=( GEOMETRIC_REPRESENTATION_CONTEXT ( 3 ) GLOBAL_UNCERTAINTY_ASSIGNED_CONTEXT ( ( #7035 ) ) GLOBAL_UNIT_ASSIGNED_CONTEXT ( ( #18526, #4015, #13710 ) ) REPRESENTATION_CONTEXT ( 'NONE', 'WORKASPACE' ) );
#16819=DIRECTION ( 'NONE',  ( -0.000000000000000000, -0.000000000000000000, 1.000000000000000000 ) ) ;
#16820=DIRECTION ( 'NONE',  ( -1.000000000000000000, 0.000000000000000000, -0.000000000000000000 ) ) ;
#16822=CARTESIAN_POINT ( 'NONE',  ( 0.000000000000000000, 0.000000000000000000, 250.0000000000000000 ) ) ;
#16824=DIRECTION ( 'NONE',  ( 1.000000000000000000, 5.889072920838430686E-16, -0.000000000000000000 ) ) ;
#16828=DIRECTION ( 'NONE',  ( 1.000000000000000000, 2.135044278125300850E-16, -0.000000000000000000 ) ) ;
#16834=EDGE_CURVE ( 'NONE', #2874, #19410, #20234, .T. ) ;
#16835=ORIENTED_EDGE ( 'NONE', *, *, #14982, .F. ) ;
#16841=VERTEX_POINT ( 'NONE', #15407 ) ;
#16843=SURFACE_SIDE_STYLE ('',( #12100 ) ) ;
#16856=ADVANCED_FACE ( 'NONE', ( #6232 ), #20328, .T. ) ;
#16869=CARTESIAN_POINT ( 'NONE',  ( 153.4893729001366864, 103.1299228374914492, 220.6387154965113382 ) ) ;
#16873=FACE_OUTER_BOUND ( 'NONE', #4494, .T. ) ;
#16876=AXIS2_PLACEMENT_3D ( 'NONE', #19251, #8516, #3588 ) ;
#16884=VECTOR ( 'NONE', #10942, 1000.000000000000000 ) ;
#16886=ORIENTED_EDGE ( 'NONE', *, *, #2045, .T. ) ;
#16900=ORIENTED_EDGE ( 'NONE', *, *, #14519, .T. ) ;
#16902=CYLINDRICAL_SURFACE ( 'NONE', #1838, 10.00000000000000888 ) ;
#16908=MECHANICAL_DESIGN_GEOMETRIC_PRESENTATION_REPRESENTATION('',(#4391),#17533);
#16917=CARTESIAN_POINT ( 'NONE',  ( 53.48937290013660828, 34.32473510485366575, 0.000000000000000000 ) ) ;
#16922=MECHANICAL_DESIGN_GEOMETRIC_PRESENTATION_REPRESENTATION('',(#15269),#1097);
#16931=PLANE ( 'NONE',  #3768 ) ;
#16940=ORIENTED_EDGE ( 'NONE', *, *, #10636, .F. ) ;
#16941=VECTOR ( 'NONE', #3013, 1000.000000000000000 ) ;
#16948=CIRCLE ( 'NONE', #10688, 10.00000000000000888 ) ;
#16955=DIRECTION ( 'NONE',  ( 0.000000000000000000, 1.000000000000000000, 0.000000000000000000 ) ) ;
#16956=ORIENTED_EDGE ( 'NONE', *, *, #7759, .T. ) ;
#16962=ORIENTED_EDGE ( 'NONE', *, *, #6494, .F. ) ;
#16963=PRESENTATION_STYLE_ASSIGNMENT (( #16558 ) ) ;
#16997=ORIENTED_EDGE ( 'NONE', *, *, #8756, .F. ) ;
#17009=PLANE ( 'NONE',  #18123 ) ;
#17018=EDGE_LOOP ( 'NONE', ( #5766, #7574, #3880, #5532 ) ) ;
#17019=VERTEX_POINT ( 'NONE', #6856 ) ;
#17021=LINE ( 'NONE', #4542, #525 ) ;
#17022=FILL_AREA_STYLE_COLOUR ( '', #7691 ) ;
#17024=DIRECTION ( 'NONE',  ( 0.000000000000000000, 0.000000000000000000, -1.000000000000000000 ) ) ;
#17036=CARTESIAN_POINT ( 'NONE',  ( -211.5106270998635409, 123.1299228374912644, 220.6387154965113382 ) ) ;
#17058=CARTESIAN_POINT ( 'NONE',  ( 133.4893729001365443, 113.1299228374914634, 79.58252780074349175 ) ) ;
#17068=CARTESIAN_POINT ( 'NONE',  ( 178.4893729001365443, 145.9162550801369491, 0.000000000000000000 ) ) ;
#17074=PLANE ( 'NONE',  #12495 ) ;
#17076=CARTESIAN_POINT ( 'NONE',  ( 78.48937290013660117, 103.1299228374914065, 29.36128450348865471 ) ) ;
#17084=DIRECTION ( 'NONE',  ( 1.000000000000000000, 5.889072920838430686E-16, -0.000000000000000000 ) ) ;
#17085=MECHANICAL_DESIGN_GEOMETRIC_PRESENTATION_REPRESENTATION('',(#2590),#10836);
#17090=SURFACE_STYLE_USAGE ( .BOTH. , #19863 ) ;
#17096=ORIENTED_EDGE ( 'NONE', *, *, #16650, .T. ) ;
#17100=ORIENTED_EDGE ( 'NONE', *, *, #3857, .T. ) ;
#17103=SURFACE_SIDE_STYLE ('',( #10823 ) ) ;
#17109=( NAMED_UNIT ( * ) SI_UNIT ( $, .STERADIAN. ) SOLID_ANGLE_UNIT ( ) );
#17110=AXIS2_PLACEMENT_3D ( 'NONE', #17233, #6125, #12289 ) ;
#17115=FILL_AREA_STYLE ('',( #13825 ) ) ;
#17116=FILL_AREA_STYLE_COLOUR ( '', #6091 ) ;
#17126=DIRECTION ( 'NONE',  ( -1.000000000000000000, -2.135044278125301096E-16, -0.000000000000000000 ) ) ;
#17133=CIRCLE ( 'NONE', #18439, 10.00000000000000888 ) ;
#17139=FILL_AREA_STYLE_COLOUR ( '', #25 ) ;
#17146=ORIENTED_EDGE ( 'NONE', *, *, #14145, .T. ) ;
#17160=ORIENTED_EDGE ( 'NONE', *, *, #791, .F. ) ;
#17162=DIRECTION ( 'NONE',  ( -1.000000000000000000, -1.595148023886719315E-16, 0.000000000000000000 ) ) ;
#17165=CARTESIAN_POINT ( 'NONE',  ( 78.48937290013662960, 1.675782865040797740E-14, 0.000000000000000000 ) ) ;
#17178=CARTESIAN_POINT ( 'NONE',  ( -211.5106270998635409, 123.1299228374912644, 220.6387154965113382 ) ) ;
#17194=AXIS2_PLACEMENT_3D ( 'NONE', #19613, #5222, #16264 ) ;
#17208=ORIENTED_EDGE ( 'NONE', *, *, #10572, .F. ) ;
#17214=DIRECTION ( 'NONE',  ( 0.000000000000000000, 0.000000000000000000, -1.000000000000000000 ) ) ;
#17215=LINE ( 'NONE', #7453, #6364 ) ;
#17218=CARTESIAN_POINT ( 'NONE',  ( 98.48937290013662960, 113.1299228374914350, 220.6387154965113382 ) ) ;
#17221=DIRECTION ( 'NONE',  ( 0.000000000000000000, 1.000000000000000000, -0.000000000000000000 ) ) ;
#17225=AXIS2_PLACEMENT_3D ( 'NONE', #11338, #4956, #8356 ) ;
#17232=ORIENTED_EDGE ( 'NONE', *, *, #10541, .T. ) ;
#17233=CARTESIAN_POINT ( 'NONE',  ( 133.4893729001365728, 0.000000000000000000, -97.94896630388704750 ) ) ;
#17235=CARTESIAN_POINT ( 'NONE',  ( 178.4893729001365443, 145.9162550801369491, 250.0000000000000000 ) ) ;
#17240=VECTOR ( 'NONE', #16647, 1000.000000000000000 ) ;
#17253=VERTEX_POINT ( 'NONE', #19139 ) ;
#17256=ORIENTED_EDGE ( 'NONE', *, *, #10094, .T. ) ;
#17262=LINE ( 'NONE', #1787, #19871 ) ;
#17278=DIRECTION ( 'NONE',  ( 1.000000000000000000, 5.889072920838430686E-16, -0.000000000000000000 ) ) ;
#17279=COLOUR_RGB ( '', 0.72549020, 0.75294118, 0.79215686) ;
#17313=ORIENTED_EDGE ( 'NONE', *, *, #3445, .F. ) ;
#17333=ORIENTED_EDGE ( 'NONE', *, *, #8799, .T. ) ;
#17334=DIRECTION ( 'NONE',  ( 0.000000000000000000, 1.000000000000000000, 0.000000000000000000 ) ) ;
#17335=ORIENTED_EDGE ( 'NONE', *, *, #8756, .T. ) ;
#17340=SURFACE_SIDE_STYLE ('',( #6848 ) ) ;
#17349=FILL_AREA_STYLE ('',( #17139 ) ) ;
#17360=MECHANICAL_DESIGN_GEOMETRIC_PRESENTATION_REPRESENTATION('',(#12101),#18992);
#17362=CARTESIAN_POINT ( 'NONE',  ( 143.0892156028631348, 80.91625508013694912, 250.0000000000000000 ) ) ;
#17366=DIRECTION ( 'NONE',  ( 0.000000000000000000, -1.000000000000000000, 0.000000000000000000 ) ) ;
#17376=DIRECTION ( 'NONE',  ( -1.595148023886719315E-16, 1.000000000000000000, -0.000000000000000000 ) ) ;
#17377=DIRECTION ( 'NONE',  ( 0.000000000000000000, -1.000000000000000000, 0.000000000000000000 ) ) ;
#17379=CARTESIAN_POINT ( 'NONE',  ( 0.000000000000000000, 80.91625508013694912, 0.000000000000000000 ) ) ;
#17390=FACE_OUTER_BOUND ( 'NONE', #4189, .T. ) ;
#17400=ORIENTED_EDGE ( 'NONE', *, *, #4195, .T. ) ;
#17403=ORIENTED_EDGE ( 'NONE', *, *, #2184, .T. ) ;
#17418=VERTEX_POINT ( 'NONE', #8628 ) ;
#17425=CYLINDRICAL_SURFACE ( 'NONE', #4966, 10.00000000000000888 ) ;
#17427=PLANE ( 'NONE',  #16634 ) ;
#17433=DIRECTION ( 'NONE',  ( -1.000000000000000000, -2.135044278125301096E-16, -0.000000000000000000 ) ) ;
#17461=EDGE_CURVE ( 'NONE', #16534, #5524, #10278, .T. ) ;
#17463=SURFACE_SIDE_STYLE ('',( #6785 ) ) ;
#17483=( NAMED_UNIT ( * ) PLANE_ANGLE_UNIT ( ) SI_UNIT ( $, .RADIAN. ) );
#17504=SURFACE_STYLE_FILL_AREA ( #5266 ) ;
#17514=DIRECTION ( 'NONE',  ( -0.000000000000000000, -0.000000000000000000, 1.000000000000000000 ) ) ;
#17519=ORIENTED_EDGE ( 'NONE', *, *, #15093, .T. ) ;
#17526=ORIENTED_EDGE ( 'NONE', *, *, #2971, .T. ) ;
#17533=( GEOMETRIC_REPRESENTATION_CONTEXT ( 3 ) GLOBAL_UNCERTAINTY_ASSIGNED_CONTEXT ( ( #18316 ) ) GLOBAL_UNIT_ASSIGNED_CONTEXT ( ( #18525, #13709, #10500 ) ) REPRESENTATION_CONTEXT ( 'NONE', 'WORKASPACE' ) );
#17540=VERTEX_POINT ( 'NONE', #20041 ) ;
#17558=FACE_BOUND ( 'NONE', #3951, .T. ) ;
#17562=CARTESIAN_POINT ( 'NONE',  ( -211.5106270998635409, 123.1299228374912644, 79.58252780074349175 ) ) ;
#17564=FILL_AREA_STYLE ('',( #14381 ) ) ;
#17565=CARTESIAN_POINT ( 'NONE',  ( -211.5106270998635409, 103.1299228374912360, 170.4174721992565082 ) ) ;
#17570=VECTOR ( 'NONE', #697, 1000.000000000000000 ) ;
#17571=EDGE_LOOP ( 'NONE', ( #13076, #557, #3859, #9645, #16886, #6630, #19089, #9883 ) ) ;
#17574=( NAMED_UNIT ( * ) PLANE_ANGLE_UNIT ( ) SI_UNIT ( $, .RADIAN. ) );
#17585=EDGE_LOOP ( 'NONE', ( #16940, #5883, #2761, #13081 ) ) ;
#17589=VERTEX_POINT ( 'NONE', #20353 ) ;
#17594=CYLINDRICAL_SURFACE ( 'NONE', #5101, 10.00000000000000888 ) ;
#17600=CARTESIAN_POINT ( 'NONE',  ( -211.5106270998635409, 123.1299228374912644, 29.36128450348865471 ) ) ;
#17601=AXIS2_PLACEMENT_3D ( 'NONE', #12988, #14721, #10084 ) ;
#17602=DIRECTION ( 'NONE',  ( 0.000000000000000000, -1.000000000000000000, 0.000000000000000000 ) ) ;
#17606=CARTESIAN_POINT ( 'NONE',  ( 153.4893729001366864, 113.1299228374914634, 170.4174721992565082 ) ) ;
#17642=( NAMED_UNIT ( * ) SI_UNIT ( $, .STERADIAN. ) SOLID_ANGLE_UNIT ( ) );
#17650=ADVANCED_FACE ( 'NONE', ( #19323 ), #663, .T. ) ;
#17658=SURFACE_STYLE_USAGE ( .BOTH. , #5398 ) ;
#17673=ORIENTED_EDGE ( 'NONE', *, *, #15828, .F. ) ;
#17676=CARTESIAN_POINT ( 'NONE',  ( 78.48937290013660117, 145.9162550801369491, -97.94896630388704750 ) ) ;
#17684=CARTESIAN_POINT ( 'NONE',  ( 153.4893729001366864, 103.1299228374914492, 79.58252780074349175 ) ) ;
#17688=ORIENTED_EDGE ( 'NONE', *, *, #7017, .T. ) ;
#17692=EDGE_LOOP ( 'NONE', ( #4580, #11765, #8517, #14187 ) ) ;
#17701=FACE_BOUND ( 'NONE', #13054, .T. ) ;
#17707=DIRECTION ( 'NONE',  ( 1.000000000000000000, 2.135044278125300850E-16, -0.000000000000000000 ) ) ;
#17732=( GEOMETRIC_REPRESENTATION_CONTEXT ( 3 ) GLOBAL_UNCERTAINTY_ASSIGNED_CONTEXT ( ( #19400 ) ) GLOBAL_UNIT_ASSIGNED_CONTEXT ( ( #10454, #13952, #945 ) ) REPRESENTATION_CONTEXT ( 'NONE', 'WORKASPACE' ) );
#17737=EDGE_LOOP ( 'NONE', ( #1823, #1570 ) ) ;
#17741=( NAMED_UNIT ( * ) PLANE_ANGLE_UNIT ( ) SI_UNIT ( $, .RADIAN. ) );
#17742=DIRECTION ( 'NONE',  ( 1.000000000000000000, 5.889072920838430686E-16, -0.000000000000000000 ) ) ;
#17744=ORIENTED_EDGE ( 'NONE', *, *, #10751, .F. ) ;
#17747=( LENGTH_UNIT ( ) NAMED_UNIT ( * ) SI_UNIT ( .MILLI., .METRE. ) );
#17756=DIRECTION ( 'NONE',  ( 0.000000000000000000, 0.000000000000000000, -1.000000000000000000 ) ) ;
#17767=LINE ( 'NONE', #14876, #8645 ) ;
#17768=ORIENTED_EDGE ( 'NONE', *, *, #15801, .T. ) ;
#17773=PLANE ( 'NONE',  #6241 ) ;
#17780=DIRECTION ( 'NONE',  ( 0.000000000000000000, -0.000000000000000000, 1.000000000000000000 ) ) ;
#17784=AXIS2_PLACEMENT_3D ( 'NONE', #4897, #10591, #20052 ) ;
#17786=ADVANCED_FACE ( 'NONE', ( #4079 ), #12022, .F. ) ;
#17801=COLOUR_RGB ( '', 0.66274510, 0.83137255, 0.94901961) ;
#17806=SURFACE_SIDE_STYLE ('',( #8448 ) ) ;
#17811=VERTEX_POINT ( 'NONE', #19921 ) ;
#17820=DIRECTION ( 'NONE',  ( -0.000000000000000000, -0.000000000000000000, 1.000000000000000000 ) ) ;
#17823=EDGE_CURVE ( 'NONE', #18834, #16767, #7009, .T. ) ;
#17827=CARTESIAN_POINT ( 'NONE',  ( 78.48937290013660117, 113.1299228374914208, 220.6387154965113382 ) ) ;
#17834=ORIENTED_EDGE ( 'NONE', *, *, #6765, .T. ) ;
#17837=LINE ( 'NONE', #8473, #7728 ) ;
#17847=DIRECTION ( 'NONE',  ( 1.000000000000000000, 5.889072920838430686E-16, -0.000000000000000000 ) ) ;
#17853=ORIENTED_EDGE ( 'NONE', *, *, #19145, .T. ) ;
#17854=CARTESIAN_POINT ( 'NONE',  ( -211.5106270998635409, 113.1299228374912502, 79.58252780074349175 ) ) ;
#17855=VECTOR ( 'NONE', #9821, 1000.000000000000000 ) ;
#17861=ORIENTED_EDGE ( 'NONE', *, *, #1540, .F. ) ;
#17866=SURFACE_STYLE_USAGE ( .BOTH. , #19690 ) ;
#17875=VERTEX_POINT ( 'NONE', #6336 ) ;
#17878=( LENGTH_UNIT ( ) NAMED_UNIT ( * ) SI_UNIT ( .MILLI., .METRE. ) );
#17882=COLOUR_RGB ( '', 0.31764706, 0.68627451, 0.89019608) ;
#17905=VECTOR ( 'NONE', #926, 1000.000000000000000 ) ;
#17912=AXIS2_PLACEMENT_3D ( 'NONE', #7355, #1026, #13833 ) ;
#17923=CARTESIAN_POINT ( 'NONE',  ( 78.48937290013660117, 113.1299228374914208, 220.6387154965113382 ) ) ;
#17926=CARTESIAN_POINT ( 'NONE',  ( 153.4893729001366580, 145.9162550801369491, -140.0000000000001137 ) ) ;
#17928=MECHANICAL_DESIGN_GEOMETRIC_PRESENTATION_REPRESENTATION('',(#6427),#13029);
#17931=DIRECTION ( 'NONE',  ( 1.000000000000000000, 2.135044278125300850E-16, -0.000000000000000000 ) ) ;
#17935=AXIS2_PLACEMENT_3D ( 'NONE', #7175, #10146, #562 ) ;
#17941=UNCERTAINTY_MEASURE_WITH_UNIT (LENGTH_MEASURE( 1.000000000000000082E-05 ), #19896, 'distance_accuracy_value', 'NONE');
#17952=FILL_AREA_STYLE ('',( #11466 ) ) ;
#17954=MECHANICAL_DESIGN_GEOMETRIC_PRESENTATION_REPRESENTATION('',(#4801),#16341);
#17965=VERTEX_POINT ( 'NONE', #8192 ) ;
#17972=CIRCLE ( 'NONE', #19296, 10.00000000000000888 ) ;
#17976=( NAMED_UNIT ( * ) SI_UNIT ( $, .STERADIAN. ) SOLID_ANGLE_UNIT ( ) );
#17977=COLOUR_RGB ( '', 0.40784314, 0.44705882, 0.49803922) ;
#18004=UNCERTAINTY_MEASURE_WITH_UNIT (LENGTH_MEASURE( 1.000000000000000082E-05 ), #8674, 'distance_accuracy_value', 'NONE');
#18006=DIRECTION ( 'NONE',  ( 0.000000000000000000, -0.000000000000000000, -1.000000000000000000 ) ) ;
#18008=VECTOR ( 'NONE', #5267, 1000.000000000000000 ) ;
#18010=ORIENTED_EDGE ( 'NONE', *, *, #14654, .T. ) ;
#18022=LINE ( 'NONE', #13210, #18008 ) ;
#18025=DIRECTION ( 'NONE',  ( 0.000000000000000000, -1.000000000000000000, 0.000000000000000000 ) ) ;
#18032=ORIENTED_EDGE ( 'NONE', *, *, #5106, .T. ) ;
#18034=SURFACE_SIDE_STYLE ('',( #5284 ) ) ;
#18042=( NAMED_UNIT ( * ) PLANE_ANGLE_UNIT ( ) SI_UNIT ( $, .RADIAN. ) );
#18057=CARTESIAN_POINT ( 'NONE',  ( 78.48937290013660117, 103.1299228374914065, 170.4174721992565082 ) ) ;
#18060=DIRECTION ( 'NONE',  ( 1.000000000000000000, 5.889072920838430686E-16, -0.000000000000000000 ) ) ;
#18072=( GEOMETRIC_REPRESENTATION_CONTEXT ( 3 ) GLOBAL_UNCERTAINTY_ASSIGNED_CONTEXT ( ( #13289 ) ) GLOBAL_UNIT_ASSIGNED_CONTEXT ( ( #10789, #5602, #15187 ) ) REPRESENTATION_CONTEXT ( 'NONE', 'WORKASPACE' ) );
#18100=( GEOMETRIC_REPRESENTATION_CONTEXT ( 3 ) GLOBAL_UNCERTAINTY_ASSIGNED_CONTEXT ( ( #686 ) ) GLOBAL_UNIT_ASSIGNED_CONTEXT ( ( #915, #5489, #12083 ) ) REPRESENTATION_CONTEXT ( 'NONE', 'WORKASPACE' ) );
#18106=DIRECTION ( 'NONE',  ( 0.000000000000000000, 1.000000000000000000, 0.000000000000000000 ) ) ;
#18109=DIRECTION ( 'NONE',  ( 1.000000000000000000, 2.135044278125300850E-16, -0.000000000000000000 ) ) ;
#18122=VERTEX_POINT ( 'NONE', #16690 ) ;
#18123=AXIS2_PLACEMENT_3D ( 'NONE', #1288, #1684, #15957 ) ;
#18126=ORIENTED_EDGE ( 'NONE', *, *, #12709, .F. ) ;
#18131=DIRECTION ( 'NONE',  ( 1.000000000000000000, 5.889072920838430686E-16, -0.000000000000000000 ) ) ;
#18154=UNCERTAINTY_MEASURE_WITH_UNIT (LENGTH_MEASURE( 1.000000000000000082E-05 ), #17747, 'distance_accuracy_value', 'NONE');
#18156=CARTESIAN_POINT ( 'NONE',  ( 133.4893729001365728, 167.9162550801369491, 250.0000000000000000 ) ) ;
#18164=CIRCLE ( 'NONE', #20133, 10.00000000000000888 ) ;
#18179=ORIENTED_EDGE ( 'NONE', *, *, #7607, .T. ) ;
#18182=ORIENTED_EDGE ( 'NONE', *, *, #1549, .T. ) ;
#18183=DIRECTION ( 'NONE',  ( 1.000000000000000000, 0.000000000000000000, 0.000000000000000000 ) ) ;
#18184=CIRCLE ( 'NONE', #8967, 10.00000000000000888 ) ;
#18188=EDGE_CURVE ( 'NONE', #17540, #6961, #3374, .T. ) ;
#18206=( GEOMETRIC_REPRESENTATION_CONTEXT ( 3 ) GLOBAL_UNCERTAINTY_ASSIGNED_CONTEXT ( ( #1001 ) ) GLOBAL_UNIT_ASSIGNED_CONTEXT ( ( #13552, #2615, #947 ) ) REPRESENTATION_CONTEXT ( 'NONE', 'WORKASPACE' ) );
#18238=ORIENTED_EDGE ( 'NONE', *, *, #18703, .F. ) ;
#18239=EDGE_LOOP ( 'NONE', ( #4165, #17096, #17100, #1991 ) ) ;
#18246=STYLED_ITEM ( 'NONE', ( #7766 ), #10481 ) ;
#18260=( NAMED_UNIT ( * ) SI_UNIT ( $, .STERADIAN. ) SOLID_ANGLE_UNIT ( ) );
#18264=AXIS2_PLACEMENT_3D ( 'NONE', #15869, #6382, #5152 ) ;
#18285=PRODUCT_CONTEXT ( 'NONE', #9860, 'mechanical' ) ;
#18287=CARTESIAN_POINT ( 'NONE',  ( -211.5106270998635409, 113.1299228374912502, 220.6387154965113382 ) ) ;
#18316=UNCERTAINTY_MEASURE_WITH_UNIT (LENGTH_MEASURE( 1.000000000000000082E-05 ), #18525, 'distance_accuracy_value', 'NONE');
#18319=FACE_BOUND ( 'NONE', #12421, .T. ) ;
#18343=AXIS2_PLACEMENT_3D ( 'NONE', #17606, #9778, #16088 ) ;
#18344=LINE ( 'NONE', #12266, #15857 ) ;
#18356=LINE ( 'NONE', #19787, #783 ) ;
#18361=FILL_AREA_STYLE_COLOUR ( '', #1273 ) ;
#18364=PLANE ( 'NONE',  #19521 ) ;
#18373=CARTESIAN_POINT ( 'NONE',  ( 53.48937290013658696, 113.1299228374914065, 170.4174721992565082 ) ) ;
#18388=LINE ( 'NONE', #9224, #10525 ) ;
#18393=FACE_BOUND ( 'NONE', #13563, .T. ) ;
#18396=AXIS2_PLACEMENT_3D ( 'NONE', #6558, #15647, #11396 ) ;
#18402=FILL_AREA_STYLE_COLOUR ( '', #3288 ) ;
#18406=EDGE_CURVE ( 'NONE', #15108, #7485, #11278, .T. ) ;
#18412=EDGE_LOOP ( 'NONE', ( #6062, #15968 ) ) ;
#18414=( NAMED_UNIT ( * ) PLANE_ANGLE_UNIT ( ) SI_UNIT ( $, .RADIAN. ) );
#18417=CARTESIAN_POINT ( 'NONE',  ( -211.5106270998635409, 113.1299228374912502, 79.58252780074349175 ) ) ;
#18418=DIRECTION ( 'NONE',  ( 1.000000000000000000, 5.889072920838430686E-16, -0.000000000000000000 ) ) ;
#18423=CARTESIAN_POINT ( 'NONE',  ( 53.48937290013660828, 34.32473510485366575, -140.0000000000001137 ) ) ;
#18438=EDGE_CURVE ( 'NONE', #10947, #11436, #6724, .T. ) ;
#18439=AXIS2_PLACEMENT_3D ( 'NONE', #2167, #11772, #14750 ) ;
#18445=CARTESIAN_POINT ( 'NONE',  ( 53.48937290013659407, 145.9162550801369491, 0.000000000000000000 ) ) ;
#18449=DIRECTION ( 'NONE',  ( -1.000000000000000000, 0.000000000000000000, -0.000000000000000000 ) ) ;
#18462=PRESENTATION_STYLE_ASSIGNMENT (( #12186 ) ) ;
#18473=SURFACE_SIDE_STYLE ('',( #2910 ) ) ;
#18491=DIRECTION ( 'NONE',  ( 1.000000000000000000, 5.889072920838430686E-16, -0.000000000000000000 ) ) ;
#18494=DIRECTION ( 'NONE',  ( 0.000000000000000000, 1.000000000000000000, 0.000000000000000000 ) ) ;
#18497=CARTESIAN_POINT ( 'NONE',  ( -211.5106270998635409, 123.1299228374912644, 220.6387154965113382 ) ) ;
#18499=LINE ( 'NONE', #12221, #8655 ) ;
#18511=ORIENTED_EDGE ( 'NONE', *, *, #5977, .T. ) ;
#18522=SURFACE_SIDE_STYLE ('',( #7127 ) ) ;
#18525=( LENGTH_UNIT ( ) NAMED_UNIT ( * ) SI_UNIT ( .MILLI., .METRE. ) );
#18526=( LENGTH_UNIT ( ) NAMED_UNIT ( * ) SI_UNIT ( .MILLI., .METRE. ) );
#18527=AXIS2_PLACEMENT_3D ( 'NONE', #6276, #70, #15863 ) ;
#18544=PLANE ( 'NONE',  #2967 ) ;
#18546=SURFACE_STYLE_USAGE ( .BOTH. , #11132 ) ;
#18552=DIRECTION ( 'NONE',  ( 0.000000000000000000, 0.000000000000000000, 1.000000000000000000 ) ) ;
#18553=DIRECTION ( 'NONE',  ( 0.000000000000000000, -1.000000000000000000, 0.000000000000000000 ) ) ;
#18557=DIRECTION ( 'NONE',  ( 1.000000000000000000, 0.000000000000000000, 0.000000000000000000 ) ) ;
#18576=( NAMED_UNIT ( * ) PLANE_ANGLE_UNIT ( ) SI_UNIT ( $, .RADIAN. ) );
#18587=SURFACE_STYLE_USAGE ( .BOTH. , #7273 ) ;
#18591=VECTOR ( 'NONE', #11110, 1000.000000000000000 ) ;
#18592=EDGE_CURVE ( 'NONE', #17811, #12058, #18499, .T. ) ;
#18597=ORIENTED_EDGE ( 'NONE', *, *, #3627, .F. ) ;
#18599=EDGE_CURVE ( 'NONE', #6961, #17540, #19175, .T. ) ;
#18608=DIRECTION ( 'NONE',  ( 1.000000000000000000, 0.000000000000000000, 0.000000000000000000 ) ) ;
#18610=CARTESIAN_POINT ( 'NONE',  ( 82.88953019741013861, 80.91625508013694912, 250.0000000000000000 ) ) ;
#18621=PRESENTATION_STYLE_ASSIGNMENT (( #15341 ) ) ;
#18627=ORIENTED_EDGE ( 'NONE', *, *, #4038, .F. ) ;
#18636=CARTESIAN_POINT ( 'NONE',  ( 78.48937290013660117, 145.9162550801369491, 250.0000000000000000 ) ) ;
#18639=DIRECTION ( 'NONE',  ( 1.000000000000000000, -0.000000000000000000, 0.000000000000000000 ) ) ;
#18640=ORIENTED_EDGE ( 'NONE', *, *, #16735, .T. ) ;
#18657=CARTESIAN_POINT ( 'NONE',  ( 143.0892156028631348, 80.91625508013694912, 250.0000000000000000 ) ) ;
#18661=DIRECTION ( 'NONE',  ( 0.000000000000000000, 1.000000000000000000, 0.000000000000000000 ) ) ;
#18665=SURFACE_STYLE_FILL_AREA ( #6515 ) ;
#18699=DIRECTION ( 'NONE',  ( 0.000000000000000000, 1.000000000000000000, 0.000000000000000000 ) ) ;
#18703=EDGE_CURVE ( 'NONE', #16028, #12290, #4908, .T. ) ;
#18707=EDGE_CURVE ( 'NONE', #3672, #19445, #19196, .T. ) ;
#18708=DIRECTION ( 'NONE',  ( 0.000000000000000000, 0.000000000000000000, 1.000000000000000000 ) ) ;
#18721=MECHANICAL_DESIGN_GEOMETRIC_PRESENTATION_REPRESENTATION('',(#3965),#339);
#18737=( GEOMETRIC_REPRESENTATION_CONTEXT ( 3 ) GLOBAL_UNCERTAINTY_ASSIGNED_CONTEXT ( ( #13220 ) ) GLOBAL_UNIT_ASSIGNED_CONTEXT ( ( #5455, #14813, #14724 ) ) REPRESENTATION_CONTEXT ( 'NONE', 'WORKASPACE' ) );
#18743=ORIENTED_EDGE ( 'NONE', *, *, #11177, .T. ) ;
#18760=AXIS2_PLACEMENT_3D ( 'NONE', #7131, #19864, #16801 ) ;
#18761=( GEOMETRIC_REPRESENTATION_CONTEXT ( 3 ) GLOBAL_UNCERTAINTY_ASSIGNED_CONTEXT ( ( #7466 ) ) GLOBAL_UNIT_ASSIGNED_CONTEXT ( ( #12633, #7988, #9436 ) ) REPRESENTATION_CONTEXT ( 'NONE', 'WORKASPACE' ) );
#18764=DIRECTION ( 'NONE',  ( 1.000000000000000000, 5.889072920838430686E-16, -0.000000000000000000 ) ) ;
#18768=( NAMED_UNIT ( * ) PLANE_ANGLE_UNIT ( ) SI_UNIT ( $, .RADIAN. ) );
#18777=LINE ( 'NONE', #15512, #16941 ) ;
#18796=SURFACE_STYLE_USAGE ( .BOTH. , #4811 ) ;
#18799=DIRECTION ( 'NONE',  ( -1.000000000000000000, -1.595148023886719315E-16, 0.000000000000000000 ) ) ;
#18802=CARTESIAN_POINT ( 'NONE',  ( 53.48937290013659407, 0.000000000000000000, 250.0000000000000000 ) ) ;
#18834=VERTEX_POINT ( 'NONE', #17684 ) ;
#18836=( GEOMETRIC_REPRESENTATION_CONTEXT ( 3 ) GLOBAL_UNCERTAINTY_ASSIGNED_CONTEXT ( ( #13035 ) ) GLOBAL_UNIT_ASSIGNED_CONTEXT ( ( #11182, #20343, #12846 ) ) REPRESENTATION_CONTEXT ( 'NONE', 'WORKASPACE' ) );
#18839=ORIENTED_EDGE ( 'NONE', *, *, #6015, .F. ) ;
#18848=SURFACE_STYLE_FILL_AREA ( #10829 ) ;
#18855=AXIS2_PLACEMENT_3D ( 'NONE', #8856, #14010, #16714 ) ;
#18856=CARTESIAN_POINT ( 'NONE',  ( 149.0892156028631348, 80.91625508013694912, 245.0000000000000000 ) ) ;
#18858=AXIS2_PLACEMENT_3D ( 'NONE', #6206, #4861, #17214 ) ;
#18862=FACE_OUTER_BOUND ( 'NONE', #11107, .T. ) ;
#18866=ORIENTED_EDGE ( 'NONE', *, *, #3903, .T. ) ;
#18883=EDGE_LOOP ( 'NONE', ( #10856, #7163, #1669, #6875 ) ) ;
#18887=EDGE_LOOP ( 'NONE', ( #244, #7179, #13088, #20072 ) ) ;
#18888=VECTOR ( 'NONE', #8944, 1000.000000000000000 ) ;
#18893=AXIS2_PLACEMENT_3D ( 'NONE', #11763, #993, #5666 ) ;
#18904=SURFACE_STYLE_FILL_AREA ( #17564 ) ;
#18911=ADVANCED_FACE ( 'NONE', ( #8716 ), #16370, .T. ) ;
#18915=LINE ( 'NONE', #6263, #4450 ) ;
#18917=ORIENTED_EDGE ( 'NONE', *, *, #1034, .T. ) ;
#18918=VECTOR ( 'NONE', #8008, 1000.000000000000000 ) ;
#18926=ORIENTED_EDGE ( 'NONE', *, *, #1002, .T. ) ;
#18929=ADVANCED_FACE ( 'NONE', ( #2303 ), #8597, .F. ) ;
#18931=DIRECTION ( 'NONE',  ( -1.000000000000000000, -0.000000000000000000, -0.000000000000000000 ) ) ;
#18945=VERTEX_POINT ( 'NONE', #4187 ) ;
#18952=( NAMED_UNIT ( * ) PLANE_ANGLE_UNIT ( ) SI_UNIT ( $, .RADIAN. ) );
#18967=EDGE_LOOP ( 'NONE', ( #14370, #5345, #17256, #1466 ) ) ;
#18970=ORIENTED_EDGE ( 'NONE', *, *, #8382, .F. ) ;
#18986=DIRECTION ( 'NONE',  ( 0.000000000000000000, 0.000000000000000000, -1.000000000000000000 ) ) ;
#18992=( GEOMETRIC_REPRESENTATION_CONTEXT ( 3 ) GLOBAL_UNCERTAINTY_ASSIGNED_CONTEXT ( ( #3193 ) ) GLOBAL_UNIT_ASSIGNED_CONTEXT ( ( #8681, #18042, #8480 ) ) REPRESENTATION_CONTEXT ( 'NONE', 'WORKASPACE' ) );
#18998=PRESENTATION_STYLE_ASSIGNMENT (( #18796 ) ) ;
#19004=LINE ( 'NONE', #4910, #1765 ) ;
#19009=CIRCLE ( 'NONE', #20337, 10.00000000000000888 ) ;
#19012=DIRECTION ( 'NONE',  ( 0.000000000000000000, 0.000000000000000000, 1.000000000000000000 ) ) ;
#19019=LINE ( 'NONE', #12558, #18591 ) ;
#19042=ADVANCED_FACE ( 'NONE', ( #9604 ), #4885, .F. ) ;
#19051=DIRECTION ( 'NONE',  ( -0.000000000000000000, -0.000000000000000000, 1.000000000000000000 ) ) ;
#19053=COLOUR_RGB ( '', 0.72549020, 0.75294118, 0.79215686) ;
#19054=ORIENTED_EDGE ( 'NONE', *, *, #18703, .T. ) ;
#19066=SURFACE_STYLE_FILL_AREA ( #12713 ) ;
#19089=ORIENTED_EDGE ( 'NONE', *, *, #7319, .T. ) ;
#19091=ORIENTED_EDGE ( 'NONE', *, *, #7710, .T. ) ;
#19097=ORIENTED_EDGE ( 'NONE', *, *, #791, .T. ) ;
#19101=PRESENTATION_STYLE_ASSIGNMENT (( #12627 ) ) ;
#19105=COLOUR_RGB ( '', 0.31764706, 0.68627451, 0.89019608) ;
#19134=AXIS2_PLACEMENT_3D ( 'NONE', #4463, #18183, #15015 ) ;
#19138=DIRECTION ( 'NONE',  ( 0.000000000000000000, -1.000000000000000000, 0.000000000000000000 ) ) ;
#19139=CARTESIAN_POINT ( 'NONE',  ( 153.4893729001366580, 80.91625508013694912, 0.000000000000000000 ) ) ;
#19140=SURFACE_STYLE_USAGE ( .BOTH. , #17806 ) ;
#19145=EDGE_CURVE ( 'NONE', #11813, #2874, #7702, .T. ) ;
#19148=ORIENTED_EDGE ( 'NONE', *, *, #12594, .T. ) ;
#19158=( NAMED_UNIT ( * ) SI_UNIT ( $, .STERADIAN. ) SOLID_ANGLE_UNIT ( ) );
#19175=CIRCLE ( 'NONE', #1378, 10.00000000000000888 ) ;
#19189=FACE_OUTER_BOUND ( 'NONE', #18887, .T. ) ;
#19191=DIRECTION ( 'NONE',  ( 1.000000000000000000, 5.889072920838430686E-16, -0.000000000000000000 ) ) ;
#19196=CIRCLE ( 'NONE', #13306, 10.00000000000000888 ) ;
#19197=( NAMED_UNIT ( * ) SI_UNIT ( $, .STERADIAN. ) SOLID_ANGLE_UNIT ( ) );
#19198=ADVANCED_FACE ( 'NONE', ( #6952 ), #547, .F. ) ;
#19202=EDGE_CURVE ( 'NONE', #345, #5312, #19682, .T. ) ;
#19210=EDGE_CURVE ( 'NONE', #17253, #5436, #15389, .T. ) ;
#19211=SURFACE_STYLE_FILL_AREA ( #11387 ) ;
#19216=DIRECTION ( 'NONE',  ( 1.000000000000000000, 5.889072920838430686E-16, -0.000000000000000000 ) ) ;
#19219=COLOUR_RGB ( '', 0.09019608, 0.27058824, 0.51372549) ;
#19233=VECTOR ( 'NONE', #14473, 1000.000000000000000 ) ;
#19244=VECTOR ( 'NONE', #11301, 1000.000000000000000 ) ;
#19245=ORIENTED_EDGE ( 'NONE', *, *, #12809, .F. ) ;
#19249=ORIENTED_EDGE ( 'NONE', *, *, #7129, .F. ) ;
#19251=CARTESIAN_POINT ( 'NONE',  ( 98.48937290013662960, 113.1299228374914350, 170.4174721992565082 ) ) ;
#19252=EDGE_CURVE ( 'NONE', #5436, #16841, #18356, .T. ) ;
#19255=DIRECTION ( 'NONE',  ( 1.000000000000000000, 5.889072920838430686E-16, -0.000000000000000000 ) ) ;
#19263=DIRECTION ( 'NONE',  ( -0.000000000000000000, -0.000000000000000000, 1.000000000000000000 ) ) ;
#19265=CARTESIAN_POINT ( 'NONE',  ( 178.4893729001365728, 103.1299228374914776, 220.6387154965113382 ) ) ;
#19266=VERTEX_POINT ( 'NONE', #2503 ) ;
#19271=ORIENTED_EDGE ( 'NONE', *, *, #5353, .F. ) ;
#19277=CIRCLE ( 'NONE', #6443, 10.00000000000000888 ) ;
#19279=( LENGTH_UNIT ( ) NAMED_UNIT ( * ) SI_UNIT ( .MILLI., .METRE. ) );
#19294=PLANE ( 'NONE',  #20247 ) ;
#19296=AXIS2_PLACEMENT_3D ( 'NONE', #601, #10188, #19449 ) ;
#19309=VERTEX_POINT ( 'NONE', #217 ) ;
#19322=ADVANCED_FACE ( 'NONE', ( #6313 ), #9582, .F. ) ;
#19323=FACE_OUTER_BOUND ( 'NONE', #16099, .T. ) ;
#19339=CARTESIAN_POINT ( 'NONE',  ( -0.000000000000000000, 167.9162550801369491, 250.0000000000000000 ) ) ;
#19342=LINE ( 'NONE', #9975, #9144 ) ;
#19350=ORIENTED_EDGE ( 'NONE', *, *, #8849, .F. ) ;
#19360=CARTESIAN_POINT ( 'NONE',  ( 153.4893729001366580, 145.9162550801369491, -140.0000000000001137 ) ) ;
#19365=CARTESIAN_POINT ( 'NONE',  ( 153.4893729001366864, 113.1299228374914634, 170.4174721992565082 ) ) ;
#19378=PLANE ( 'NONE',  #11873 ) ;
#19382=DIRECTION ( 'NONE',  ( 0.000000000000000000, 0.000000000000000000, -1.000000000000000000 ) ) ;
#19396=ORIENTED_EDGE ( 'NONE', *, *, #8997, .F. ) ;
#19400=UNCERTAINTY_MEASURE_WITH_UNIT (LENGTH_MEASURE( 1.000000000000000082E-05 ), #10454, 'distance_accuracy_value', 'NONE');
#19401=DIRECTION ( 'NONE',  ( 1.000000000000000000, 2.135044278125300850E-16, -0.000000000000000000 ) ) ;
#19408=PRESENTATION_STYLE_ASSIGNMENT (( #2405 ) ) ;
#19410=VERTEX_POINT ( 'NONE', #13930 ) ;
#19411=SURFACE_STYLE_FILL_AREA ( #8421 ) ;
#19414=FILL_AREA_STYLE_COLOUR ( '', #11970 ) ;
#19445=VERTEX_POINT ( 'NONE', #313 ) ;
#19446=ORIENTED_EDGE ( 'NONE', *, *, #8799, .F. ) ;
#19449=DIRECTION ( 'NONE',  ( 0.000000000000000000, 1.000000000000000000, 0.000000000000000000 ) ) ;
#19455=FACE_BOUND ( 'NONE', #15037, .T. ) ;
#19466=EDGE_LOOP ( 'NONE', ( #1470, #15627, #5302, #14228, #17768, #7467 ) ) ;
#19468=SURFACE_STYLE_USAGE ( .BOTH. , #18034 ) ;
#19470=MECHANICAL_DESIGN_GEOMETRIC_PRESENTATION_REPRESENTATION('',(#7974),#9590);
#19490=ORIENTED_EDGE ( 'NONE', *, *, #5977, .F. ) ;
#19494=LINE ( 'NONE', #2284, #12307 ) ;
#19501=FACE_OUTER_BOUND ( 'NONE', #6031, .T. ) ;
#19506=DIRECTION ( 'NONE',  ( -0.000000000000000000, 0.000000000000000000, 1.000000000000000000 ) ) ;
#19511=ORIENTED_EDGE ( 'NONE', *, *, #14451, .F. ) ;
#19514=VECTOR ( 'NONE', #3041, 1000.000000000000000 ) ;
#19521=AXIS2_PLACEMENT_3D ( 'NONE', #7359, #1031, #13645 ) ;
#19531=STYLED_ITEM ( 'NONE', ( #2272 ), #19198 ) ;
#19543=ORIENTED_EDGE ( 'NONE', *, *, #15906, .F. ) ;
#19544=EDGE_CURVE ( 'NONE', #1665, #11661, #14842, .T. ) ;
#19545=ORIENTED_EDGE ( 'NONE', *, *, #2045, .F. ) ;
#19546=ORIENTED_EDGE ( 'NONE', *, *, #15550, .F. ) ;
#19551=CARTESIAN_POINT ( 'NONE',  ( -211.5106270998635409, 113.1299228374912502, 170.4174721992565082 ) ) ;
#19569=AXIS2_PLACEMENT_3D ( 'NONE', #2903, #1454, #4877 ) ;
#19572=VERTEX_POINT ( 'NONE', #9906 ) ;
#19584=LINE ( 'NONE', #5491, #1772 ) ;
#19586=DIRECTION ( 'NONE',  ( 0.000000000000000000, 1.000000000000000000, 0.000000000000000000 ) ) ;
#19587=DIRECTION ( 'NONE',  ( 1.000000000000000000, 5.889072920838430686E-16, -0.000000000000000000 ) ) ;
#19600=EDGE_CURVE ( 'NONE', #3926, #5312, #7083, .T. ) ;
#19602=UNCERTAINTY_MEASURE_WITH_UNIT (LENGTH_MEASURE( 1.000000000000000082E-05 ), #5486, 'distance_accuracy_value', 'NONE');
#19603=CIRCLE ( 'NONE', #10098, 10.00000000000000888 ) ;
#19609=FILL_AREA_STYLE_COLOUR ( '', #17279 ) ;
#19613=CARTESIAN_POINT ( 'NONE',  ( 153.4893729001366864, 113.1299228374914634, 79.58252780074349175 ) ) ;
#19615=SURFACE_STYLE_USAGE ( .BOTH. , #13376 ) ;
#19617=ORIENTED_EDGE ( 'NONE', *, *, #14654, .F. ) ;
#19625=LINE ( 'NONE', #5533, #794 ) ;
#19636=UNCERTAINTY_MEASURE_WITH_UNIT (LENGTH_MEASURE( 1.000000000000000082E-05 ), #9297, 'distance_accuracy_value', 'NONE');
#19673=CARTESIAN_POINT ( 'NONE',  ( 0.000000000000000000, 80.91625508013694912, 250.0000000000000000 ) ) ;
#19675=CARTESIAN_POINT ( 'NONE',  ( 78.48937290013660117, 123.1299228374914208, 170.4174721992565082 ) ) ;
#19677=AXIS2_PLACEMENT_3D ( 'NONE', #9201, #10651, #16955 ) ;
#19682=LINE ( 'NONE', #16743, #17240 ) ;
#19690=SURFACE_SIDE_STYLE ('',( #13452 ) ) ;
#19695=FACE_OUTER_BOUND ( 'NONE', #4697, .T. ) ;
#19703=DIRECTION ( 'NONE',  ( -0.000000000000000000, -0.000000000000000000, 1.000000000000000000 ) ) ;
#19705=AXIS2_PLACEMENT_3D ( 'NONE', #7110, #16191, #9784 ) ;
#19707=AXIS2_PLACEMENT_3D ( 'NONE', #16753, #6963, #13245 ) ;
#19720=ORIENTED_EDGE ( 'NONE', *, *, #19252, .F. ) ;
#19726=CARTESIAN_POINT ( 'NONE',  ( 178.4893729001365728, 123.1299228374914918, 79.58252780074349175 ) ) ;
#19742=ORIENTED_EDGE ( 'NONE', *, *, #2217, .F. ) ;
#19755=CARTESIAN_POINT ( 'NONE',  ( -211.5106270998635409, 113.1299228374912502, 170.4174721992565082 ) ) ;
#19764=VECTOR ( 'NONE', #12695, 1000.000000000000000 ) ;
#19769=CARTESIAN_POINT ( 'NONE',  ( -211.5106270998635409, 113.1299228374912502, 29.36128450348865471 ) ) ;
#19771=CARTESIAN_POINT ( 'NONE',  ( 78.48937290013661539, 80.91625508013694912, 250.0000000000000000 ) ) ;
#19773=( NAMED_UNIT ( * ) SI_UNIT ( $, .STERADIAN. ) SOLID_ANGLE_UNIT ( ) );
#19777=EDGE_CURVE ( 'NONE', #15658, #6311, #6755, .T. ) ;
#19787=CARTESIAN_POINT ( 'NONE',  ( 153.4893729001366580, 145.9162550801369491, -97.94896630388704750 ) ) ;
#19788=ADVANCED_FACE ( 'NONE', ( #11256 ), #14758, .F. ) ;
#19790=UNCERTAINTY_MEASURE_WITH_UNIT (LENGTH_MEASURE( 1.000000000000000082E-05 ), #13701, 'distance_accuracy_value', 'NONE');
#19800=VECTOR ( 'NONE', #14097, 1000.000000000000000 ) ;
#19802=LINE ( 'NONE', #15095, #9398 ) ;
#19813=( NAMED_UNIT ( * ) PLANE_ANGLE_UNIT ( ) SI_UNIT ( $, .RADIAN. ) );
#19818=VECTOR ( 'NONE', #5685, 1000.000000000000000 ) ;
#19822=DIRECTION ( 'NONE',  ( 9.815121534730717399E-17, -1.000000000000000000, 0.000000000000000000 ) ) ;
#19833=AXIS2_PLACEMENT_3D ( 'NONE', #11313, #378, #15576 ) ;
#19834=DIRECTION ( 'NONE',  ( 1.000000000000000000, 5.889072920838430686E-16, -0.000000000000000000 ) ) ;
#19852=AXIS2_PLACEMENT_3D ( 'NONE', #9942, #19401, #16152 ) ;
#19859=CARTESIAN_POINT ( 'NONE',  ( 98.48937290013660117, 167.9162550801369491, 0.000000000000000000 ) ) ;
#19863=SURFACE_SIDE_STYLE ('',( #10713 ) ) ;
#19864=DIRECTION ( 'NONE',  ( 0.000000000000000000, 1.000000000000000000, -0.000000000000000000 ) ) ;
#19866=COLOUR_RGB ( '', 0.08235294, 0.09019608, 0.10196078) ;
#19871=VECTOR ( 'NONE', #7882, 1000.000000000000000 ) ;
#19876=DIRECTION ( 'NONE',  ( 1.000000000000000000, 5.889072920838430686E-16, -0.000000000000000000 ) ) ;
#19896=( LENGTH_UNIT ( ) NAMED_UNIT ( * ) SI_UNIT ( .MILLI., .METRE. ) );
#19902=CIRCLE ( 'NONE', #10063, 10.00000000000000888 ) ;
#19908=FILL_AREA_STYLE_COLOUR ( '', #10656 ) ;
#19909=VECTOR ( 'NONE', #1756, 1000.000000000000000 ) ;
#19911=DIRECTION ( 'NONE',  ( 0.000000000000000000, 0.000000000000000000, 1.000000000000000000 ) ) ;
#19917=SHAPE_DEFINITION_REPRESENTATION ( #1307, #3934 ) ;
#19921=CARTESIAN_POINT ( 'NONE',  ( 133.4893729001365728, 167.9162550801369491, 0.000000000000000000 ) ) ;
#19951=VERTEX_POINT ( 'NONE', #19675 ) ;
#19953=FACE_BOUND ( 'NONE', #1953, .T. ) ;
#19960=DIRECTION ( 'NONE',  ( 1.000000000000000000, 5.889072920838430686E-16, -0.000000000000000000 ) ) ;
#19963=( LENGTH_UNIT ( ) NAMED_UNIT ( * ) SI_UNIT ( .MILLI., .METRE. ) );
#19982=UNCERTAINTY_MEASURE_WITH_UNIT (LENGTH_MEASURE( 1.000000000000000082E-05 ), #8059, 'distance_accuracy_value', 'NONE');
#20001=EDGE_LOOP ( 'NONE', ( #19245, #14298, #3292, #14539 ) ) ;
#20003=PRESENTATION_STYLE_ASSIGNMENT (( #2705 ) ) ;
#20013=DIRECTION ( 'NONE',  ( 0.000000000000000000, 1.000000000000000000, 0.000000000000000000 ) ) ;
#20025=STYLED_ITEM ( 'NONE', ( #383 ), #16227 ) ;
#20031=CARTESIAN_POINT ( 'NONE',  ( 133.4893729001365443, 123.1299228374914634, 220.6387154965113382 ) ) ;
#20032=( GEOMETRIC_REPRESENTATION_CONTEXT ( 3 ) GLOBAL_UNCERTAINTY_ASSIGNED_CONTEXT ( ( #7174 ) ) GLOBAL_UNIT_ASSIGNED_CONTEXT ( ( #12636, #3356, #256 ) ) REPRESENTATION_CONTEXT ( 'NONE', 'WORKASPACE' ) );
#20040=FILL_AREA_STYLE_COLOUR ( '', #19053 ) ;
#20041=CARTESIAN_POINT ( 'NONE',  ( 98.48937290013662960, 123.1299228374914350, 29.36128450348865471 ) ) ;
#20052=DIRECTION ( 'NONE',  ( 0.000000000000000000, -1.000000000000000000, 0.000000000000000000 ) ) ;
#20061=CARTESIAN_POINT ( 'NONE',  ( 53.48937290013658696, 113.1299228374914065, 29.36128450348865471 ) ) ;
#20064=STYLED_ITEM ( 'NONE', ( #9525 ), #6993 ) ;
#20070=ADVANCED_FACE ( 'NONE', ( #16613 ), #2356, .F. ) ;
#20072=ORIENTED_EDGE ( 'NONE', *, *, #4238, .F. ) ;
#20083=CARTESIAN_POINT ( 'NONE',  ( 88.88953019741013861, 80.91625508013694912, 245.0000000000000000 ) ) ;
#20085=SURFACE_STYLE_USAGE ( .BOTH. , #2883 ) ;
#20091=DIRECTION ( 'NONE',  ( 1.000000000000000000, 5.889072920838430686E-16, -0.000000000000000000 ) ) ;
#20102=AXIS2_PLACEMENT_3D ( 'NONE', #7330, #7633, #5888 ) ;
#20105=ORIENTED_EDGE ( 'NONE', *, *, #14033, .F. ) ;
#20106=EDGE_CURVE ( 'NONE', #11813, #7140, #7220, .T. ) ;
#20108=VECTOR ( 'NONE', #7203, 1000.000000000000000 ) ;
#20118=VERTEX_POINT ( 'NONE', #12822 ) ;
#20120=SURFACE_SIDE_STYLE ('',( #2717 ) ) ;
#20124=ORIENTED_EDGE ( 'NONE', *, *, #3957, .F. ) ;
#20133=AXIS2_PLACEMENT_3D ( 'NONE', #9952, #13253, #14784 ) ;
#20155=ORIENTED_EDGE ( 'NONE', *, *, #12709, .T. ) ;
#20157=PRESENTATION_STYLE_ASSIGNMENT (( #4615 ) ) ;
#20163=VECTOR ( 'NONE', #19191, 1000.000000000000000 ) ;
#20171=CARTESIAN_POINT ( 'NONE',  ( 53.48937290013658696, 103.1299228374913923, 220.6387154965113382 ) ) ;
#20183=DIRECTION ( 'NONE',  ( 0.000000000000000000, 0.000000000000000000, 1.000000000000000000 ) ) ;
#20189=CARTESIAN_POINT ( 'NONE',  ( 53.48937290013660828, 34.32473510485366575, 250.0000000000000000 ) ) ;
#20190=UNCERTAINTY_MEASURE_WITH_UNIT (LENGTH_MEASURE( 1.000000000000000082E-05 ), #864, 'distance_accuracy_value', 'NONE');
#20192=ADVANCED_FACE ( 'NONE', ( #9255 ), #15459, .F. ) ;
#20202=EDGE_CURVE ( 'NONE', #243, #270, #2664, .T. ) ;
#20213=EDGE_CURVE ( 'NONE', #18834, #6655, #9069, .T. ) ;
#20215=ORIENTED_EDGE ( 'NONE', *, *, #1601, .T. ) ;
#20234=LINE ( 'NONE', #32, #12541 ) ;
#20241=EDGE_LOOP ( 'NONE', ( #16007, #4193, #852, #17688 ) ) ;
#20243=VERTEX_POINT ( 'NONE', #20171 ) ;
#20247=AXIS2_PLACEMENT_3D ( 'NONE', #722, #8476, #10214 ) ;
#20252=VECTOR ( 'NONE', #10567, 1000.000000000000000 ) ;
#20255=DIRECTION ( 'NONE',  ( 0.000000000000000000, 1.000000000000000000, 0.000000000000000000 ) ) ;
#20276=DIRECTION ( 'NONE',  ( 1.000000000000000000, 5.889072920838430686E-16, -0.000000000000000000 ) ) ;
#20287=VERTEX_POINT ( 'NONE', #14101 ) ;
#20300=DIRECTION ( 'NONE',  ( 0.000000000000000000, -1.000000000000000000, 0.000000000000000000 ) ) ;
#20305=DIRECTION ( 'NONE',  ( -1.000000000000000000, -1.595148023886719315E-16, 0.000000000000000000 ) ) ;
#20310=EDGE_CURVE ( 'NONE', #15658, #4273, #4057, .T. ) ;
#20318=CARTESIAN_POINT ( 'NONE',  ( 82.88953019741013861, 80.91625508013694912, 245.0000000000000000 ) ) ;
#20328=PLANE ( 'NONE',  #6623 ) ;
#20337=AXIS2_PLACEMENT_3D ( 'NONE', #4906, #18799, #7893 ) ;
#20343=( NAMED_UNIT ( * ) PLANE_ANGLE_UNIT ( ) SI_UNIT ( $, .RADIAN. ) );
#20352=STYLED_ITEM ( 'NONE', ( #16760 ), #4856 ) ;
#20353=CARTESIAN_POINT ( 'NONE',  ( 153.4893729001366580, 145.9162550801369491, 250.0000000000000000 ) ) ;
#20363=COLOUR_RGB ( '', 0.09019608, 0.27058824, 0.51372549) ;
ENDSEC;
END-ISO-10303-21;
